ISO-10303-21;
HEADER;
FILE_DESCRIPTION (('STEP AP214'),
    '1' );
FILE_NAME ('Servo-Bas.step',
    '2026-11-01T05:08:46',
    ( '' ),
    ( '' ),
    'SwSTEP 2.0',
    'SolidWorks 2024',
    '' );
FILE_SCHEMA (( 'AUTOMOTIVE_DESIGN' ));
ENDSEC;

DATA;
#10=CYLINDRICAL_SURFACE ( 'NONE', #6483, 2.500000000000002220 ) ;
#27=LINE ( 'NONE', #2765, #10533 ) ;
#28=ORIENTED_EDGE ( 'NONE', *, *, #16422, .T. ) ;
#34=LINE ( 'NONE', #2692, #9964 ) ;
#42=EDGE_CURVE ( 'NONE', #687, #1391, #10203, .T. ) ;
#48=VECTOR ( 'NONE', #5957, 1000.000000000000000 ) ;
#58=CARTESIAN_POINT ( 'NONE',  ( 25.99999999999996092, 3.000000000000000000, 40.00000000000000711 ) ) ;
#62=ORIENTED_EDGE ( 'NONE', *, *, #2061, .T. ) ;
#67=EDGE_CURVE ( 'NONE', #12951, #10672, #5562, .T. ) ;
#112=ORIENTED_EDGE ( 'NONE', *, *, #11806, .F. ) ;
#121=ORIENTED_EDGE ( 'NONE', *, *, #14551, .T. ) ;
#123=PLANE ( 'NONE',  #5672 ) ;
#144=CARTESIAN_POINT ( 'NONE',  ( -39.99999999999997868, 3.000000000000000000, -19.99999999999999645 ) ) ;
#157=CARTESIAN_POINT ( 'NONE',  ( 20.99999999999996092, 3.000000000000000000, 37.50000000000001421 ) ) ;
#169=CARTESIAN_POINT ( 'NONE',  ( -23.00000000000003197, 3.000000000000000000, 34.00000000000000711 ) ) ;
#175=VERTEX_POINT ( 'NONE', #3080 ) ;
#178=VECTOR ( 'NONE', #11720, 1000.000000000000000 ) ;
#201=VECTOR ( 'NONE', #6539, 1000.000000000000000 ) ;
#217=ORIENTED_EDGE ( 'NONE', *, *, #4009, .F. ) ;
#240=DIRECTION ( 'NONE',  ( -0.000000000000000000, -1.000000000000000000, -0.000000000000000000 ) ) ;
#248=CARTESIAN_POINT ( 'NONE',  ( -34.99999999999998579, 0.000000000000000000, 21.00000000000000355 ) ) ;
#272=DIRECTION ( 'NONE',  ( -1.000000000000000000, 0.000000000000000000, -1.156482317317870344E-15 ) ) ;
#287=EDGE_CURVE ( 'NONE', #1978, #13400, #16248, .T. ) ;
#300=ORIENTED_EDGE ( 'NONE', *, *, #13299, .F. ) ;
#311=LINE ( 'NONE', #16104, #13556 ) ;
#343=AXIS2_PLACEMENT_3D ( 'NONE', #9197, #13949, #2656 ) ;
#371=FACE_OUTER_BOUND ( 'NONE', #10755, .T. ) ;
#379=CIRCLE ( 'NONE', #6377, 2.500000000000002220 ) ;
#382=ADVANCED_FACE ( 'NONE', ( #2449 ), #5115, .F. ) ;
#409=EDGE_CURVE ( 'NONE', #14941, #16656, #5188, .T. ) ;
#436=VECTOR ( 'NONE', #240, 1000.000000000000000 ) ;
#449=AXIS2_PLACEMENT_3D ( 'NONE', #10426, #15659, #7844 ) ;
#452=VERTEX_POINT ( 'NONE', #15766 ) ;
#485=EDGE_CURVE ( 'NONE', #7998, #10795, #7719, .T. ) ;
#505=ORIENTED_EDGE ( 'NONE', *, *, #11806, .T. ) ;
#512=DIRECTION ( 'NONE',  ( -0.000000000000000000, -1.000000000000000000, -0.000000000000000000 ) ) ;
#521=EDGE_CURVE ( 'NONE', #10509, #13944, #4186, .T. ) ;
#522=FACE_BOUND ( 'NONE', #6433, .T. ) ;
#523=UNCERTAINTY_MEASURE_WITH_UNIT (LENGTH_MEASURE( 1.000000000000000082E-05 ), #13317, 'distance_accuracy_value', 'NONE');
#535=EDGE_CURVE ( 'NONE', #6745, #7963, #6646, .T. ) ;
#542=CARTESIAN_POINT ( 'NONE',  ( 20.99999999999996092, 3.000000000000000000, 32.50000000000000711 ) ) ;
#562=CARTESIAN_POINT ( 'NONE',  ( 25.99999999999996092, 3.000000000000000000, -33.99999999999998579 ) ) ;
#577=ADVANCED_FACE ( 'NONE', ( #8127 ), #5716, .F. ) ;
#582=VECTOR ( 'NONE', #5460, 1000.000000000000000 ) ;
#606=CARTESIAN_POINT ( 'NONE',  ( -39.99999999999997868, 0.000000000000000000, -19.99999999999999645 ) ) ;
#622=AXIS2_PLACEMENT_3D ( 'NONE', #13030, #1258, #10441 ) ;
#624=DIRECTION ( 'NONE',  ( 0.000000000000000000, 0.000000000000000000, 1.000000000000000000 ) ) ;
#628=APPLICATION_CONTEXT ( 'automotive_design' ) ;
#636=ORIENTED_EDGE ( 'NONE', *, *, #1848, .F. ) ;
#639=CYLINDRICAL_SURFACE ( 'NONE', #13237, 36.50000000000000000 ) ;
#646=VECTOR ( 'NONE', #13968, 1000.000000000000000 ) ;
#648=CARTESIAN_POINT ( 'NONE',  ( 19.99999999999995381, 3.000000000000000000, -39.99999999999999289 ) ) ;
#659=DIRECTION ( 'NONE',  ( 0.000000000000000000, 1.000000000000000000, 0.000000000000000000 ) ) ;
#668=ORIENTED_EDGE ( 'NONE', *, *, #15780, .T. ) ;
#675=DIRECTION ( 'NONE',  ( 0.000000000000000000, 0.000000000000000000, -1.000000000000000000 ) ) ;
#687=VERTEX_POINT ( 'NONE', #1861 ) ;
#707=DIRECTION ( 'NONE',  ( -0.000000000000000000, -1.000000000000000000, -0.000000000000000000 ) ) ;
#715=DIRECTION ( 'NONE',  ( -0.000000000000000000, 1.000000000000000000, -0.000000000000000000 ) ) ;
#721=FACE_OUTER_BOUND ( 'NONE', #15457, .T. ) ;
#722=EDGE_LOOP ( 'NONE', ( #12294, #300, #10535, #9049 ) ) ;
#723=LINE ( 'NONE', #880, #14088 ) ;
#732=CYLINDRICAL_SURFACE ( 'NONE', #11039, 2.500000000000002220 ) ;
#733=CARTESIAN_POINT ( 'NONE',  ( 40.00000000000003553, -20.00000000000000000, 20.00000000000000355 ) ) ;
#736=CARTESIAN_POINT ( 'NONE',  ( -26.00000000000002842, 3.000000000000000000, 34.00000000000000711 ) ) ;
#754=AXIS2_PLACEMENT_3D ( 'NONE', #13149, #16831, #1378 ) ;
#768=ORIENTED_EDGE ( 'NONE', *, *, #9538, .T. ) ;
#772=ORIENTED_EDGE ( 'NONE', *, *, #409, .F. ) ;
#817=FACE_OUTER_BOUND ( 'NONE', #12262, .T. ) ;
#819=CARTESIAN_POINT ( 'NONE',  ( 0.000000000000000000, 3.000000000000000000, 0.000000000000000000 ) ) ;
#822=CARTESIAN_POINT ( 'NONE',  ( 30.99999999999999645, 0.000000000000000000, -25.99999999999999645 ) ) ;
#827=CARTESIAN_POINT ( 'NONE',  ( -34.99999999999998579, 3.000000000000000000, 21.00000000000000355 ) ) ;
#853=ORIENTED_EDGE ( 'NONE', *, *, #7304, .F. ) ;
#856=VERTEX_POINT ( 'NONE', #16613 ) ;
#864=EDGE_LOOP ( 'NONE', ( #15035, #505 ) ) ;
#866=LINE ( 'NONE', #15115, #3690 ) ;
#879=EDGE_CURVE ( 'NONE', #5928, #11595, #14905, .T. ) ;
#880=CARTESIAN_POINT ( 'NONE',  ( -31.00000000000006750, 3.000000000000000000, 26.00000000000000355 ) ) ;
#883=AXIS2_PLACEMENT_3D ( 'NONE', #14599, #9360, #9454 ) ;
#889=CARTESIAN_POINT ( 'NONE',  ( 0.000000000000000000, 0.000000000000000000, 0.000000000000000000 ) ) ;
#897=EDGE_CURVE ( 'NONE', #9574, #11859, #6282, .T. ) ;
#929=AXIS2_PLACEMENT_3D ( 'NONE', #3641, #4997, #16603 ) ;
#942=ORIENTED_EDGE ( 'NONE', *, *, #7282, .T. ) ;
#960=DIRECTION ( 'NONE',  ( -0.000000000000000000, -1.000000000000000000, -0.000000000000000000 ) ) ;
#974=VERTEX_POINT ( 'NONE', #7921 ) ;
#994=EDGE_LOOP ( 'NONE', ( #9054, #6956, #636, #13363 ) ) ;
#1002=CARTESIAN_POINT ( 'NONE',  ( -26.00000000000002842, 3.000000000000000000, -31.00000000000003197 ) ) ;
#1006=PLANE ( 'NONE',  #2046 ) ;
#1019=EDGE_CURVE ( 'NONE', #14941, #1746, #34, .T. ) ;
#1039=EDGE_CURVE ( 'NONE', #7998, #1155, #14979, .T. ) ;
#1042=DIRECTION ( 'NONE',  ( -0.000000000000000000, -1.000000000000000000, -0.000000000000000000 ) ) ;
#1060=PLANE ( 'NONE',  #1731 ) ;
#1067=ORIENTED_EDGE ( 'NONE', *, *, #14128, .T. ) ;
#1070=ORIENTED_EDGE ( 'NONE', *, *, #15795, .F. ) ;
#1117=VECTOR ( 'NONE', #2312, 1000.000000000000000 ) ;
#1123=ORIENTED_EDGE ( 'NONE', *, *, #16120, .T. ) ;
#1137=VERTEX_POINT ( 'NONE', #2566 ) ;
#1155=VERTEX_POINT ( 'NONE', #7881 ) ;
#1160=DIRECTION ( 'NONE',  ( 0.000000000000000000, 0.000000000000000000, -1.000000000000000000 ) ) ;
#1162=EDGE_LOOP ( 'NONE', ( #6373, #8256, #3553, #16098, #13335, #4560, #4416, #2032, #9926, #13252, #5328, #6594, #4833, #1994, #6733, #6071, #7894, #4053, #11863, #14292, #4454, #11780, #768, #13512, #14863, #62, #11534, #6786 ) ) ;
#1225=ORIENTED_EDGE ( 'NONE', *, *, #10248, .T. ) ;
#1248=PLANE ( 'NONE',  #9114 ) ;
#1258=DIRECTION ( 'NONE',  ( -0.000000000000000000, -1.000000000000000000, 0.000000000000000000 ) ) ;
#1266=EDGE_CURVE ( 'NONE', #6745, #14546, #5394, .T. ) ;
#1290=LINE ( 'NONE', #3707, #3363 ) ;
#1295=FACE_OUTER_BOUND ( 'NONE', #5747, .T. ) ;
#1297=ORIENTED_EDGE ( 'NONE', *, *, #13299, .T. ) ;
#1334=CYLINDRICAL_SURFACE ( 'NONE', #4212, 2.999999999999995559 ) ;
#1338=FACE_OUTER_BOUND ( 'NONE', #8908, .T. ) ;
#1341=CARTESIAN_POINT ( 'NONE',  ( 37.00000000000003553, -20.00000000000000000, 23.00000000000000355 ) ) ;
#1360=DIRECTION ( 'NONE',  ( 0.000000000000000000, 0.000000000000000000, -1.000000000000000000 ) ) ;
#1370=CARTESIAN_POINT ( 'NONE',  ( 20.99999999999996092, 0.000000000000000000, 35.00000000000000711 ) ) ;
#1378=DIRECTION ( 'NONE',  ( 0.000000000000000000, 0.000000000000000000, -1.000000000000000000 ) ) ;
#1381=AXIS2_PLACEMENT_3D ( 'NONE', #7328, #8638, #13704 ) ;
#1389=VERTEX_POINT ( 'NONE', #11644 ) ;
#1391=VERTEX_POINT ( 'NONE', #15667 ) ;
#1393=DIRECTION ( 'NONE',  ( 0.000000000000000000, 0.000000000000000000, -1.000000000000000000 ) ) ;
#1400=CARTESIAN_POINT ( 'NONE',  ( -20.00000000000003197, 0.000000000000000000, 40.00000000000000711 ) ) ;
#1414=ADVANCED_FACE ( 'NONE', ( #12926 ), #14656, .F. ) ;
#1425=VECTOR ( 'NONE', #2460, 1000.000000000000000 ) ;
#1446=DIRECTION ( 'NONE',  ( -0.000000000000000000, 1.000000000000000000, -0.000000000000000000 ) ) ;
#1449=AXIS2_PLACEMENT_3D ( 'NONE', #3060, #14488, #9418 ) ;
#1454=EDGE_LOOP ( 'NONE', ( #112, #4903, #15639, #15666 ) ) ;
#1469=CARTESIAN_POINT ( 'NONE',  ( 20.99999999999996092, -20.00000000000000000, 35.00000000000000711 ) ) ;
#1488=AXIS2_PLACEMENT_3D ( 'NONE', #3280, #8693, #15217 ) ;
#1494=VECTOR ( 'NONE', #2847, 1000.000000000000000 ) ;
#1503=CARTESIAN_POINT ( 'NONE',  ( -20.00000000000003197, 3.000000000000000000, 40.00000000000000711 ) ) ;
#1506=VERTEX_POINT ( 'NONE', #14484 ) ;
#1507=ORIENTED_EDGE ( 'NONE', *, *, #10893, .T. ) ;
#1518=DIRECTION ( 'NONE',  ( 0.000000000000000000, 0.000000000000000000, 1.000000000000000000 ) ) ;
#1522=ORIENTED_EDGE ( 'NONE', *, *, #10341, .T. ) ;
#1524=EDGE_CURVE ( 'NONE', #12261, #1137, #6552, .T. ) ;
#1533=CARTESIAN_POINT ( 'NONE',  ( -26.00000000000002842, 0.000000000000000000, -39.99999999999999289 ) ) ;
#1535=ADVANCED_FACE ( 'NONE', ( #9325 ), #2789, .F. ) ;
#1537=LINE ( 'NONE', #14506, #12511 ) ;
#1559=DIRECTION ( 'NONE',  ( -0.000000000000000000, -1.000000000000000000, -0.000000000000000000 ) ) ;
#1567=VERTEX_POINT ( 'NONE', #11034 ) ;
#1574=DIRECTION ( 'NONE',  ( -0.000000000000000000, -0.000000000000000000, 1.000000000000000000 ) ) ;
#1576=DIRECTION ( 'NONE',  ( -0.000000000000000000, 1.000000000000000000, -0.000000000000000000 ) ) ;
#1583=FACE_OUTER_BOUND ( 'NONE', #11974, .T. ) ;
#1586=CARTESIAN_POINT ( 'NONE',  ( 34.00000000000002842, 3.000000000000000000, 26.00000000000000355 ) ) ;
#1591=VECTOR ( 'NONE', #12521, 1000.000000000000000 ) ;
#1598=DIRECTION ( 'NONE',  ( -0.000000000000000000, 1.000000000000000000, -0.000000000000000000 ) ) ;
#1604=CARTESIAN_POINT ( 'NONE',  ( 19.99999999999995381, 3.000000000000000000, -36.99999999999999289 ) ) ;
#1605=VERTEX_POINT ( 'NONE', #9583 ) ;
#1613=DIRECTION ( 'NONE',  ( 0.000000000000000000, 0.000000000000000000, -1.000000000000000000 ) ) ;
#1647=EDGE_LOOP ( 'NONE', ( #12569, #2644, #3350, #4243 ) ) ;
#1664=CARTESIAN_POINT ( 'NONE',  ( 19.99999999999995381, 3.000000000000000000, -39.99999999999999289 ) ) ;
#1692=CARTESIAN_POINT ( 'NONE',  ( -39.99999999999997868, -20.00000000000000000, -19.99999999999999645 ) ) ;
#1700=CARTESIAN_POINT ( 'NONE',  ( -21.00000000000002842, 0.000000000000000000, -34.99999999999999289 ) ) ;
#1717=LINE ( 'NONE', #5900, #6701 ) ;
#1725=ORIENTED_EDGE ( 'NONE', *, *, #3322, .F. ) ;
#1731=AXIS2_PLACEMENT_3D ( 'NONE', #16127, #4659, #3075 ) ;
#1736=VECTOR ( 'NONE', #14208, 1000.000000000000000 ) ;
#1746=VERTEX_POINT ( 'NONE', #11276 ) ;
#1759=VERTEX_POINT ( 'NONE', #7482 ) ;
#1789=DIRECTION ( 'NONE',  ( -1.156482317317870344E-15, 0.000000000000000000, 1.000000000000000000 ) ) ;
#1792=DIRECTION ( 'NONE',  ( 0.000000000000000000, 0.000000000000000000, -1.000000000000000000 ) ) ;
#1818=VECTOR ( 'NONE', #15289, 1000.000000000000000 ) ;
#1829=ADVANCED_FACE ( 'NONE', ( #14443 ), #12036, .F. ) ;
#1838=PLANE ( 'NONE',  #9977 ) ;
#1847=CARTESIAN_POINT ( 'NONE',  ( -39.99999999999997868, 3.000000000000000000, -25.99999999999999645 ) ) ;
#1848=EDGE_CURVE ( 'NONE', #10672, #10225, #16132, .T. ) ;
#1861=CARTESIAN_POINT ( 'NONE',  ( -26.00000000000002842, 3.000000000000000000, -31.00000000000003197 ) ) ;
#1862=DIRECTION ( 'NONE',  ( -1.000000000000000000, 0.000000000000000000, 0.000000000000000000 ) ) ;
#1888=ORIENTED_EDGE ( 'NONE', *, *, #3346, .F. ) ;
#1902=DIRECTION ( 'NONE',  ( -0.000000000000000000, 1.000000000000000000, -0.000000000000000000 ) ) ;
#1906=CARTESIAN_POINT ( 'NONE',  ( 35.00000000000003553, 0.000000000000000000, -20.99999999999999645 ) ) ;
#1925=DIRECTION ( 'NONE',  ( 0.000000000000000000, 1.000000000000000000, 0.000000000000000000 ) ) ;
#1978=VERTEX_POINT ( 'NONE', #7196 ) ;
#1994=ORIENTED_EDGE ( 'NONE', *, *, #12802, .F. ) ;
#2011=ORIENTED_EDGE ( 'NONE', *, *, #10862, .F. ) ;
#2023=ORIENTED_EDGE ( 'NONE', *, *, #535, .F. ) ;
#2032=ORIENTED_EDGE ( 'NONE', *, *, #6664, .T. ) ;
#2033=CARTESIAN_POINT ( 'NONE',  ( -39.99999999999997868, -20.00000000000000000, -19.99999999999999645 ) ) ;
#2045=VERTEX_POINT ( 'NONE', #4393 ) ;
#2046=AXIS2_PLACEMENT_3D ( 'NONE', #4775, #11301, #8655 ) ;
#2051=EDGE_CURVE ( 'NONE', #2088, #13185, #16401, .T. ) ;
#2061=EDGE_CURVE ( 'NONE', #16656, #11956, #15320, .T. ) ;
#2069=PRODUCT_CONTEXT ( 'NONE', #628, 'mechanical' ) ;
#2072=CARTESIAN_POINT ( 'NONE',  ( -23.00000000000003197, 3.000000000000000000, 34.00000000000000711 ) ) ;
#2082=ORIENTED_EDGE ( 'NONE', *, *, #9538, .F. ) ;
#2088=VERTEX_POINT ( 'NONE', #8759 ) ;
#2089=CARTESIAN_POINT ( 'NONE',  ( 25.99999999999996092, 0.000000000000000000, 31.00000000000004263 ) ) ;
#2091=CARTESIAN_POINT ( 'NONE',  ( 37.00000000000003553, -20.00000000000000000, 20.00000000000000000 ) ) ;
#2134=ORIENTED_EDGE ( 'NONE', *, *, #3086, .F. ) ;
#2146=SHAPE_DEFINITION_REPRESENTATION ( #8090, #12316 ) ;
#2148=SHAPE_REPRESENTATION_RELATIONSHIP ( 'NONE' , 'NONE' ,  #12316, #11622 ) ;
#2163=ORIENTED_EDGE ( 'NONE', *, *, #4790, .T. ) ;
#2172=CARTESIAN_POINT ( 'NONE',  ( 25.99999999999996092, 0.000000000000000000, 40.00000000000000711 ) ) ;
#2174=CIRCLE ( 'NONE', #14527, 4.999999999999997335 ) ;
#2185=EDGE_CURVE ( 'NONE', #10598, #974, #14079, .T. ) ;
#2191=ORIENTED_EDGE ( 'NONE', *, *, #2269, .F. ) ;
#2196=DIRECTION ( 'NONE',  ( -0.000000000000000000, -1.000000000000000000, -0.000000000000000000 ) ) ;
#2209=CARTESIAN_POINT ( 'NONE',  ( 25.99999999999996092, 3.000000000000000000, -31.00000000000003197 ) ) ;
#2219=ORIENTED_EDGE ( 'NONE', *, *, #10037, .T. ) ;
#2225=EDGE_CURVE ( 'NONE', #9633, #11217, #5440, .T. ) ;
#2238=ADVANCED_FACE ( 'NONE', ( #10878 ), #14329, .F. ) ;
#2263=ORIENTED_EDGE ( 'NONE', *, *, #12358, .F. ) ;
#2269=EDGE_CURVE ( 'NONE', #9495, #13726, #15598, .T. ) ;
#2277=CIRCLE ( 'NONE', #3929, 4.999999999999997335 ) ;
#2297=DIRECTION ( 'NONE',  ( 0.000000000000000000, 1.000000000000000000, 0.000000000000000000 ) ) ;
#2312=DIRECTION ( 'NONE',  ( 0.000000000000000000, 0.000000000000000000, -1.000000000000000000 ) ) ;
#2327=ORIENTED_EDGE ( 'NONE', *, *, #7806, .T. ) ;
#2350=ORIENTED_EDGE ( 'NONE', *, *, #10641, .F. ) ;
#2353=DIRECTION ( 'NONE',  ( -0.000000000000000000, -1.000000000000000000, -0.000000000000000000 ) ) ;
#2362=EDGE_CURVE ( 'NONE', #8007, #14343, #6818, .T. ) ;
#2371=APPLICATION_CONTEXT ( 'automotive_design' ) ;
#2384=ORIENTED_EDGE ( 'NONE', *, *, #12010, .T. ) ;
#2411=ORIENTED_EDGE ( 'NONE', *, *, #16716, .T. ) ;
#2416=ORIENTED_EDGE ( 'NONE', *, *, #10060, .T. ) ;
#2439=PLANE ( 'NONE',  #6907 ) ;
#2449=FACE_OUTER_BOUND ( 'NONE', #10149, .T. ) ;
#2460=DIRECTION ( 'NONE',  ( -1.000000000000000000, -0.000000000000000000, -1.156482317317870344E-15 ) ) ;
#2465=DIRECTION ( 'NONE',  ( 0.000000000000000000, 0.000000000000000000, 1.000000000000000000 ) ) ;
#2490=DIRECTION ( 'NONE',  ( -0.000000000000000000, 1.000000000000000000, -0.000000000000000000 ) ) ;
#2495=DIRECTION ( 'NONE',  ( 0.000000000000000000, 0.000000000000000000, -1.000000000000000000 ) ) ;
#2508=AXIS2_PLACEMENT_3D ( 'NONE', #8631, #11119, #9835 ) ;
#2510=ORIENTED_EDGE ( 'NONE', *, *, #1039, .T. ) ;
#2517=CIRCLE ( 'NONE', #11026, 2.500000000000002220 ) ;
#2523=VERTEX_POINT ( 'NONE', #1400 ) ;
#2526=FACE_BOUND ( 'NONE', #12867, .T. ) ;
#2564=FILL_AREA_STYLE ('',( #16899 ) ) ;
#2566=CARTESIAN_POINT ( 'NONE',  ( -36.99999999999997868, 3.000000000000000000, -19.99999999999999289 ) ) ;
#2575=PLANE ( 'NONE',  #343 ) ;
#2608=CYLINDRICAL_SURFACE ( 'NONE', #10612, 3.000000000000002665 ) ;
#2623=ORIENTED_EDGE ( 'NONE', *, *, #42, .F. ) ;
#2644=ORIENTED_EDGE ( 'NONE', *, *, #2867, .F. ) ;
#2646=EDGE_CURVE ( 'NONE', #1389, #687, #13092, .T. ) ;
#2648=DIRECTION ( 'NONE',  ( -0.000000000000000000, -1.000000000000000000, -0.000000000000000000 ) ) ;
#2656=DIRECTION ( 'NONE',  ( -1.000000000000000000, 0.000000000000000000, -0.000000000000000000 ) ) ;
#2665=DIRECTION ( 'NONE',  ( 0.000000000000000000, 0.000000000000000000, 1.000000000000000000 ) ) ;
#2692=CARTESIAN_POINT ( 'NONE',  ( 25.99999999999996092, 3.000000000000000000, 40.00000000000000711 ) ) ;
#2699=ADVANCED_FACE ( 'NONE', ( #4415 ), #1838, .F. ) ;
#2733=ORIENTED_EDGE ( 'NONE', *, *, #4142, .T. ) ;
#2737=DIRECTION ( 'NONE',  ( 0.000000000000000000, 0.000000000000000000, -1.000000000000000000 ) ) ;
#2765=CARTESIAN_POINT ( 'NONE',  ( 40.00000000000003553, 3.000000000000000000, 26.00000000000000355 ) ) ;
#2768=EDGE_CURVE ( 'NONE', #1605, #7341, #9307, .T. ) ;
#2776=ORIENTED_EDGE ( 'NONE', *, *, #11307, .F. ) ;
#2787=AXIS2_PLACEMENT_3D ( 'NONE', #15221, #960, #624 ) ;
#2789=PLANE ( 'NONE',  #4711 ) ;
#2800=CYLINDRICAL_SURFACE ( 'NONE', #9442, 4.999999999999997335 ) ;
#2817=DIRECTION ( 'NONE',  ( 0.000000000000000000, 0.000000000000000000, -1.000000000000000000 ) ) ;
#2820=VECTOR ( 'NONE', #15102, 1000.000000000000000 ) ;
#2826=AXIS2_PLACEMENT_3D ( 'NONE', #3209, #9480, #9651 ) ;
#2827=LINE ( 'NONE', #3001, #9595 ) ;
#2828=EDGE_CURVE ( 'NONE', #1155, #5033, #9150, .T. ) ;
#2832=VECTOR ( 'NONE', #13543, 1000.000000000000000 ) ;
#2842=VECTOR ( 'NONE', #9030, 1000.000000000000000 ) ;
#2847=DIRECTION ( 'NONE',  ( -0.000000000000000000, -1.000000000000000000, -0.000000000000000000 ) ) ;
#2867=EDGE_CURVE ( 'NONE', #974, #15821, #723, .T. ) ;
#2904=ORIENTED_EDGE ( 'NONE', *, *, #6395, .F. ) ;
#2922=DIRECTION ( 'NONE',  ( 0.000000000000000000, 0.000000000000000000, -1.000000000000000000 ) ) ;
#2927=VECTOR ( 'NONE', #14686, 1000.000000000000000 ) ;
#2935=CARTESIAN_POINT ( 'NONE',  ( -33.99999999999997158, -20.00000000000000000, -22.99999999999999645 ) ) ;
#2946=PLANE ( 'NONE',  #11635 ) ;
#2963=DIRECTION ( 'NONE',  ( -0.000000000000000000, -1.000000000000000000, -0.000000000000000000 ) ) ;
#2969=CARTESIAN_POINT ( 'NONE',  ( 22.99999999999995737, 3.000000000000000000, -33.99999999999998579 ) ) ;
#2984=ADVANCED_FACE ( 'NONE', ( #11600 ), #5230, .F. ) ;
#3001=CARTESIAN_POINT ( 'NONE',  ( 22.99999999999995737, 0.000000000000000000, -33.99999999999998579 ) ) ;
#3017=EDGE_CURVE ( 'NONE', #14546, #3021, #13425, .T. ) ;
#3021=VERTEX_POINT ( 'NONE', #4317 ) ;
#3048=DIRECTION ( 'NONE',  ( -0.000000000000000000, -1.000000000000000000, -0.000000000000000000 ) ) ;
#3054=CARTESIAN_POINT ( 'NONE',  ( 40.00000000000003553, 0.000000000000000000, 26.00000000000000355 ) ) ;
#3060=CARTESIAN_POINT ( 'NONE',  ( 20.99999999999996092, 3.000000000000000000, 35.00000000000000711 ) ) ;
#3075=DIRECTION ( 'NONE',  ( 0.000000000000000000, 0.000000000000000000, 1.000000000000000000 ) ) ;
#3079=LINE ( 'NONE', #14847, #2927 ) ;
#3080=CARTESIAN_POINT ( 'NONE',  ( 40.00000000000003553, 3.000000000000000000, -25.99999999999999645 ) ) ;
#3081=CIRCLE ( 'NONE', #14048, 2.500000000000002220 ) ;
#3086=EDGE_CURVE ( 'NONE', #11696, #452, #15034, .T. ) ;
#3101=DIRECTION ( 'NONE',  ( -0.000000000000000000, -1.000000000000000000, 0.000000000000000000 ) ) ;
#3131=DIRECTION ( 'NONE',  ( 0.000000000000000000, 0.000000000000000000, -1.000000000000000000 ) ) ;
#3134=LINE ( 'NONE', #16730, #4591 ) ;
#3147=EDGE_CURVE ( 'NONE', #8007, #1605, #9727, .T. ) ;
#3152=FACE_OUTER_BOUND ( 'NONE', #16754, .T. ) ;
#3184=DIRECTION ( 'NONE',  ( 0.000000000000000000, 0.000000000000000000, 1.000000000000000000 ) ) ;
#3187=ORIENTED_EDGE ( 'NONE', *, *, #11715, .F. ) ;
#3188=LINE ( 'NONE', #13915, #16296 ) ;
#3205=DIRECTION ( 'NONE',  ( -0.000000000000000000, -1.000000000000000000, -0.000000000000000000 ) ) ;
#3208=ORIENTED_EDGE ( 'NONE', *, *, #16835, .T. ) ;
#3209=CARTESIAN_POINT ( 'NONE',  ( 0.000000000000000000, 16.00000000000000000, 0.000000000000000000 ) ) ;
#3216=EDGE_CURVE ( 'NONE', #10795, #5033, #13052, .T. ) ;
#3224=ORIENTED_EDGE ( 'NONE', *, *, #15611, .F. ) ;
#3237=EDGE_CURVE ( 'NONE', #856, #9116, #14082, .T. ) ;
#3244=MANIFOLD_SOLID_BREP ( 'Boss-Extrude3', #14305 ) ;
#3254=CARTESIAN_POINT ( 'NONE',  ( 0.000000000000000000, 0.000000000000000000, 0.000000000000000000 ) ) ;
#3280=CARTESIAN_POINT ( 'NONE',  ( 0.000000000000000000, 0.000000000000000000, 0.000000000000000000 ) ) ;
#3281=CYLINDRICAL_SURFACE ( 'NONE', #12882, 4.999999999999997335 ) ;
#3292=VERTEX_POINT ( 'NONE', #14591 ) ;
#3297=EDGE_CURVE ( 'NONE', #6332, #1567, #2517, .T. ) ;
#3322=EDGE_CURVE ( 'NONE', #11217, #9633, #8008, .T. ) ;
#3336=LINE ( 'NONE', #8746, #1591 ) ;
#3346=EDGE_CURVE ( 'NONE', #12951, #9574, #14421, .T. ) ;
#3350=ORIENTED_EDGE ( 'NONE', *, *, #2185, .F. ) ;
#3354=ORIENTED_EDGE ( 'NONE', *, *, #16835, .F. ) ;
#3355=VECTOR ( 'NONE', #5267, 1000.000000000000000 ) ;
#3363=VECTOR ( 'NONE', #6508, 1000.000000000000000 ) ;
#3424=ORIENTED_EDGE ( 'NONE', *, *, #16120, .F. ) ;
#3469=ORIENTED_EDGE ( 'NONE', *, *, #2768, .F. ) ;
#3475=FACE_OUTER_BOUND ( 'NONE', #12891, .T. ) ;
#3497=ADVANCED_FACE ( 'NONE', ( #4616 ), #16307, .F. ) ;
#3513=ORIENTED_EDGE ( 'NONE', *, *, #1039, .F. ) ;
#3529=ORIENTED_EDGE ( 'NONE', *, *, #13194, .F. ) ;
#3531=AXIS2_PLACEMENT_3D ( 'NONE', #11752, #10785, #9586 ) ;
#3553=ORIENTED_EDGE ( 'NONE', *, *, #15795, .T. ) ;
#3571=AXIS2_PLACEMENT_3D ( 'NONE', #15346, #6224, #3759 ) ;
#3582=FACE_OUTER_BOUND ( 'NONE', #11884, .T. ) ;
#3619=ORIENTED_EDGE ( 'NONE', *, *, #5470, .F. ) ;
#3638=ORIENTED_EDGE ( 'NONE', *, *, #485, .F. ) ;
#3641=CARTESIAN_POINT ( 'NONE',  ( -31.00000000000002842, 3.000000000000000000, 31.00000000000000000 ) ) ;
#3687=CARTESIAN_POINT ( 'NONE',  ( 4.469960816887838430E-15, 50.00000000000000000, 36.50000000000000000 ) ) ;
#3690=VECTOR ( 'NONE', #707, 1000.000000000000000 ) ;
#3691=DIRECTION ( 'NONE',  ( 1.000000000000000000, 0.000000000000000000, 0.000000000000000000 ) ) ;
#3707=CARTESIAN_POINT ( 'NONE',  ( 30.99999999999999645, 0.000000000000000000, 26.00000000000000355 ) ) ;
#3713=FACE_OUTER_BOUND ( 'NONE', #4136, .T. ) ;
#3734=ADVANCED_FACE ( 'NONE', ( #4275 ), #2800, .F. ) ;
#3736=ADVANCED_FACE ( 'NONE', ( #13294 ), #6821, .F. ) ;
#3749=CARTESIAN_POINT ( 'NONE',  ( -26.00000000000002842, 3.000000000000000000, -39.99999999999999289 ) ) ;
#3759=DIRECTION ( 'NONE',  ( 0.000000000000000000, 0.000000000000000000, -1.000000000000000000 ) ) ;
#3762=DIRECTION ( 'NONE',  ( 0.000000000000000000, 0.000000000000000000, 1.000000000000000000 ) ) ;
#3793=CARTESIAN_POINT ( 'NONE',  ( -33.99999999999997158, 0.000000000000000000, -25.99999999999999645 ) ) ;
#3797=ORIENTED_EDGE ( 'NONE', *, *, #7342, .F. ) ;
#3798=ORIENTED_EDGE ( 'NONE', *, *, #4009, .T. ) ;
#3813=CARTESIAN_POINT ( 'NONE',  ( -23.00000000000003197, 0.000000000000000000, 34.00000000000000711 ) ) ;
#3815=ADVANCED_FACE ( 'NONE', ( #4357 ), #11209, .F. ) ;
#3817=ORIENTED_EDGE ( 'NONE', *, *, #521, .F. ) ;
#3823=FACE_OUTER_BOUND ( 'NONE', #15174, .T. ) ;
#3824=DIRECTION ( 'NONE',  ( 0.000000000000000000, 0.000000000000000000, -1.000000000000000000 ) ) ;
#3844=DIRECTION ( 'NONE',  ( 0.000000000000000000, 0.000000000000000000, 1.000000000000000000 ) ) ;
#3849=VECTOR ( 'NONE', #675, 1000.000000000000000 ) ;
#3865=DIRECTION ( 'NONE',  ( -0.000000000000000000, 1.000000000000000000, -0.000000000000000000 ) ) ;
#3869=AXIS2_PLACEMENT_3D ( 'NONE', #16536, #4678, #4771 ) ;
#3879=DIRECTION ( 'NONE',  ( -0.000000000000000000, -1.000000000000000000, -0.000000000000000000 ) ) ;
#3880=VERTEX_POINT ( 'NONE', #14913 ) ;
#3900=AXIS2_PLACEMENT_3D ( 'NONE', #3254, #7349, #12598 ) ;
#3901=VECTOR ( 'NONE', #12321, 1000.000000000000000 ) ;
#3928=AXIS2_PLACEMENT_3D ( 'NONE', #6206, #15502, #14134 ) ;
#3929=AXIS2_PLACEMENT_3D ( 'NONE', #16041, #13305, #5461 ) ;
#3936=DIRECTION ( 'NONE',  ( -0.000000000000000000, -1.000000000000000000, 0.000000000000000000 ) ) ;
#3952=VECTOR ( 'NONE', #8522, 1000.000000000000000 ) ;
#3958=CARTESIAN_POINT ( 'NONE',  ( -34.99999999999998579, -20.00000000000000000, 21.00000000000000355 ) ) ;
#3966=CARTESIAN_POINT ( 'NONE',  ( 19.99999999999995381, 0.000000000000000000, -36.99999999999999289 ) ) ;
#3993=DIRECTION ( 'NONE',  ( 0.000000000000000000, 0.000000000000000000, 1.000000000000000000 ) ) ;
#4009=EDGE_CURVE ( 'NONE', #7947, #2523, #15640, .T. ) ;
#4017=CARTESIAN_POINT ( 'NONE',  ( 4.163799117101000559E-15, 23.00000000000000000, 34.00000000000000000 ) ) ;
#4024=ADVANCED_FACE ( 'NONE', ( #9924 ), #14274, .F. ) ;
#4028=ORIENTED_EDGE ( 'NONE', *, *, #9160, .F. ) ;
#4038=DIRECTION ( 'NONE',  ( 0.000000000000000000, 0.000000000000000000, -1.000000000000000000 ) ) ;
#4053=ORIENTED_EDGE ( 'NONE', *, *, #2185, .T. ) ;
#4075=DIRECTION ( 'NONE',  ( -0.000000000000000000, -1.000000000000000000, -0.000000000000000000 ) ) ;
#4078=ORIENTED_EDGE ( 'NONE', *, *, #1019, .F. ) ;
#4089=CARTESIAN_POINT ( 'NONE',  ( 25.99999999999996092, 3.000000000000000000, 31.00000000000004263 ) ) ;
#4105=DIRECTION ( 'NONE',  ( 0.000000000000000000, 0.000000000000000000, -1.000000000000000000 ) ) ;
#4106=VERTEX_POINT ( 'NONE', #14708 ) ;
#4115=CARTESIAN_POINT ( 'NONE',  ( 19.99999999999995381, 0.000000000000000000, -36.99999999999999289 ) ) ;
#4127=VERTEX_POINT ( 'NONE', #8173 ) ;
#4136=EDGE_LOOP ( 'NONE', ( #2263, #4794, #12215, #5192 ) ) ;
#4140=FACE_OUTER_BOUND ( 'NONE', #14363, .T. ) ;
#4142=EDGE_CURVE ( 'NONE', #1389, #6048, #5333, .T. ) ;
#4144=CARTESIAN_POINT ( 'NONE',  ( -36.99999999999997868, -20.00000000000000000, -19.99999999999999289 ) ) ;
#4186=CIRCLE ( 'NONE', #1449, 2.500000000000002220 ) ;
#4212=AXIS2_PLACEMENT_3D ( 'NONE', #10360, #15590, #1160 ) ;
#4213=CYLINDRICAL_SURFACE ( 'NONE', #883, 4.999999999999997335 ) ;
#4219=CARTESIAN_POINT ( 'NONE',  ( 40.00000000000003553, 0.000000000000000000, -25.99999999999999645 ) ) ;
#4243=ORIENTED_EDGE ( 'NONE', *, *, #16683, .T. ) ;
#4275=FACE_OUTER_BOUND ( 'NONE', #15391, .T. ) ;
#4280=EDGE_CURVE ( 'NONE', #10225, #7947, #866, .T. ) ;
#4296=CARTESIAN_POINT ( 'NONE',  ( 20.99999999999996092, 0.000000000000000000, 35.00000000000000711 ) ) ;
#4311=ORIENTED_EDGE ( 'NONE', *, *, #13377, .F. ) ;
#4317=CARTESIAN_POINT ( 'NONE',  ( -33.99999999999997158, 3.000000000000000000, -22.99999999999999645 ) ) ;
#4351=LINE ( 'NONE', #3054, #2832 ) ;
#4357=FACE_OUTER_BOUND ( 'NONE', #722, .T. ) ;
#4389=DIRECTION ( 'NONE',  ( -0.000000000000000000, 1.000000000000000000, -0.000000000000000000 ) ) ;
#4393=CARTESIAN_POINT ( 'NONE',  ( 40.00000000000003553, 3.000000000000000000, 20.00000000000000355 ) ) ;
#4395=ORIENTED_EDGE ( 'NONE', *, *, #15894, .T. ) ;
#4399=VECTOR ( 'NONE', #6822, 1000.000000000000000 ) ;
#4415=FACE_OUTER_BOUND ( 'NONE', #13948, .T. ) ;
#4416=ORIENTED_EDGE ( 'NONE', *, *, #2051, .T. ) ;
#4429=AXIS2_PLACEMENT_3D ( 'NONE', #10359, #15588, #3824 ) ;
#4449=DIRECTION ( 'NONE',  ( -0.000000000000000000, 1.000000000000000000, -0.000000000000000000 ) ) ;
#4454=ORIENTED_EDGE ( 'NONE', *, *, #67, .T. ) ;
#4460=CARTESIAN_POINT ( 'NONE',  ( -33.99999999999997158, 0.000000000000000000, -22.99999999999999645 ) ) ;
#4461=CIRCLE ( 'NONE', #15431, 2.500000000000002220 ) ;
#4472=CARTESIAN_POINT ( 'NONE',  ( 22.99999999999995737, 3.000000000000000000, -33.99999999999998579 ) ) ;
#4475=CARTESIAN_POINT ( 'NONE',  ( 37.00000000000003553, 0.000000000000000000, 23.00000000000000355 ) ) ;
#4483=VECTOR ( 'NONE', #12235, 1000.000000000000000 ) ;
#4485=CARTESIAN_POINT ( 'NONE',  ( 30.99999999999996092, 3.000000000000000000, -30.99999999999999289 ) ) ;
#4493=CARTESIAN_POINT ( 'NONE',  ( -23.00000000000003197, 0.000000000000000000, 34.00000000000000711 ) ) ;
#4507=AXIS2_PLACEMENT_3D ( 'NONE', #4475, #4558, #5927 ) ;
#4510=CARTESIAN_POINT ( 'NONE',  ( 0.000000000000000000, 26.00000000000000000, 0.000000000000000000 ) ) ;
#4538=DIRECTION ( 'NONE',  ( 0.000000000000000000, 1.000000000000000000, 0.000000000000000000 ) ) ;
#4558=DIRECTION ( 'NONE',  ( -0.000000000000000000, -1.000000000000000000, 0.000000000000000000 ) ) ;
#4560=ORIENTED_EDGE ( 'NONE', *, *, #6073, .T. ) ;
#4568=CARTESIAN_POINT ( 'NONE',  ( -20.00000000000003197, 3.000000000000000000, 40.00000000000000711 ) ) ;
#4576=EDGE_LOOP ( 'NONE', ( #6800, #9668, #5639, #5596 ) ) ;
#4588=LINE ( 'NONE', #1847, #3901 ) ;
#4591=VECTOR ( 'NONE', #6083, 1000.000000000000000 ) ;
#4616=FACE_OUTER_BOUND ( 'NONE', #13939, .T. ) ;
#4642=CARTESIAN_POINT ( 'NONE',  ( 35.00000000000003553, -20.00000000000000000, -20.99999999999999645 ) ) ;
#4646=ORIENTED_EDGE ( 'NONE', *, *, #2225, .T. ) ;
#4653=FACE_OUTER_BOUND ( 'NONE', #12982, .T. ) ;
#4656=CARTESIAN_POINT ( 'NONE',  ( -20.00000000000003197, 3.000000000000000000, 37.00000000000000711 ) ) ;
#4659=DIRECTION ( 'NONE',  ( -1.000000000000000000, 0.000000000000000000, 0.000000000000000000 ) ) ;
#4667=ORIENTED_EDGE ( 'NONE', *, *, #11283, .T. ) ;
#4678=DIRECTION ( 'NONE',  ( 0.000000000000000000, 0.000000000000000000, -1.000000000000000000 ) ) ;
#4698=VECTOR ( 'NONE', #14687, 1000.000000000000000 ) ;
#4704=AXIS2_PLACEMENT_3D ( 'NONE', #13433, #9383, #14878 ) ;
#4711=AXIS2_PLACEMENT_3D ( 'NONE', #16274, #9763, #12406 ) ;
#4714=VECTOR ( 'NONE', #2963, 1000.000000000000000 ) ;
#4739=CIRCLE ( 'NONE', #2826, 34.00000000000000000 ) ;
#4742=FACE_OUTER_BOUND ( 'NONE', #14114, .T. ) ;
#4771=DIRECTION ( 'NONE',  ( -1.000000000000000000, 0.000000000000000000, -0.000000000000000000 ) ) ;
#4775=CARTESIAN_POINT ( 'NONE',  ( -20.00000000000003197, 3.000000000000000000, 37.00000000000000711 ) ) ;
#4790=EDGE_CURVE ( 'NONE', #14343, #9226, #7774, .T. ) ;
#4794=ORIENTED_EDGE ( 'NONE', *, *, #3297, .T. ) ;
#4801=ORIENTED_EDGE ( 'NONE', *, *, #5632, .T. ) ;
#4823=DIRECTION ( 'NONE',  ( -0.000000000000000000, -1.000000000000000000, -0.000000000000000000 ) ) ;
#4833=ORIENTED_EDGE ( 'NONE', *, *, #14333, .T. ) ;
#4852=DIRECTION ( 'NONE',  ( 0.000000000000000000, 0.000000000000000000, 1.000000000000000000 ) ) ;
#4875=ORIENTED_EDGE ( 'NONE', *, *, #10985, .F. ) ;
#4903=ORIENTED_EDGE ( 'NONE', *, *, #5035, .T. ) ;
#4911=ORIENTED_EDGE ( 'NONE', *, *, #11307, .T. ) ;
#4934=CARTESIAN_POINT ( 'NONE',  ( 22.99999999999995737, 0.000000000000000000, -36.99999999999999289 ) ) ;
#4973=EDGE_CURVE ( 'NONE', #14275, #8711, #5358, .T. ) ;
#4975=DIRECTION ( 'NONE',  ( 0.000000000000000000, 0.000000000000000000, -1.000000000000000000 ) ) ;
#4986=CARTESIAN_POINT ( 'NONE',  ( 0.000000000000000000, 23.00000000000000000, 0.000000000000000000 ) ) ;
#4990=AXIS2_PLACEMENT_3D ( 'NONE', #889, #16600, #5140 ) ;
#4997=DIRECTION ( 'NONE',  ( -0.000000000000000000, -1.000000000000000000, 0.000000000000000000 ) ) ;
#5000=CARTESIAN_POINT ( 'NONE',  ( -26.00000000000002842, 3.000000000000000000, 31.00000000000003908 ) ) ;
#5027=AXIS2_PLACEMENT_3D ( 'NONE', #5862, #11019, #15130 ) ;
#5033=VERTEX_POINT ( 'NONE', #7864 ) ;
#5035=EDGE_CURVE ( 'NONE', #1759, #1978, #6746, .T. ) ;
#5045=VERTEX_POINT ( 'NONE', #14575 ) ;
#5068=PLANE ( 'NONE',  #15458 ) ;
#5087=CARTESIAN_POINT ( 'NONE',  ( 0.000000000000000000, 50.00000000000000000, -36.50000000000000000 ) ) ;
#5105=DIRECTION ( 'NONE',  ( -0.000000000000000000, 1.000000000000000000, -0.000000000000000000 ) ) ;
#5108=VECTOR ( 'NONE', #10368, 1000.000000000000000 ) ;
#5115=CYLINDRICAL_SURFACE ( 'NONE', #11564, 3.000000000000002665 ) ;
#5122=CARTESIAN_POINT ( 'NONE',  ( 34.00000000000002842, 3.000000000000000000, 23.00000000000000355 ) ) ;
#5140=DIRECTION ( 'NONE',  ( 0.000000000000000000, 0.000000000000000000, -1.000000000000000000 ) ) ;
#5141=ORIENTED_EDGE ( 'NONE', *, *, #2768, .T. ) ;
#5162=ADVANCED_FACE ( 'NONE', ( #12506 ), #7007, .T. ) ;
#5188=LINE ( 'NONE', #58, #5253 ) ;
#5192=ORIENTED_EDGE ( 'NONE', *, *, #12849, .T. ) ;
#5195=VECTOR ( 'NONE', #10216, 1000.000000000000000 ) ;
#5202=ORIENTED_EDGE ( 'NONE', *, *, #6462, .T. ) ;
#5203=VECTOR ( 'NONE', #1446, 1000.000000000000000 ) ;
#5230=CYLINDRICAL_SURFACE ( 'NONE', #13824, 2.500000000000002220 ) ;
#5242=LINE ( 'NONE', #15899, #16563 ) ;
#5253=VECTOR ( 'NONE', #10529, 1000.000000000000000 ) ;
#5259=EDGE_LOOP ( 'NONE', ( #12042, #6069, #9784, #3513 ) ) ;
#5267=DIRECTION ( 'NONE',  ( 1.000000000000000000, 0.000000000000000000, 1.156482317317870344E-15 ) ) ;
#5271=CYLINDRICAL_SURFACE ( 'NONE', #14557, 2.500000000000002220 ) ;
#5298=EDGE_CURVE ( 'NONE', #14722, #15314, #12240, .T. ) ;
#5328=ORIENTED_EDGE ( 'NONE', *, *, #2646, .T. ) ;
#5333=LINE ( 'NONE', #6959, #1494 ) ;
#5358=CIRCLE ( 'NONE', #12488, 4.999999999999997335 ) ;
#5382=PLANE ( 'NONE',  #13542 ) ;
#5393=DIRECTION ( 'NONE',  ( 0.000000000000000000, 1.000000000000000000, 0.000000000000000000 ) ) ;
#5394=LINE ( 'NONE', #6681, #8828 ) ;
#5401=ORIENTED_EDGE ( 'NONE', *, *, #14986, .F. ) ;
#5420=ORIENTED_EDGE ( 'NONE', *, *, #879, .T. ) ;
#5423=EDGE_CURVE ( 'NONE', #13185, #4106, #7928, .T. ) ;
#5433=LINE ( 'NONE', #14726, #12284 ) ;
#5440=CIRCLE ( 'NONE', #6253, 2.500000000000002220 ) ;
#5448=DIRECTION ( 'NONE',  ( 0.000000000000000000, 0.000000000000000000, -1.000000000000000000 ) ) ;
#5449=DIRECTION ( 'NONE',  ( 0.000000000000000000, 0.000000000000000000, 1.000000000000000000 ) ) ;
#5460=DIRECTION ( 'NONE',  ( 0.000000000000000000, 0.000000000000000000, 1.000000000000000000 ) ) ;
#5461=DIRECTION ( 'NONE',  ( 0.000000000000000000, 0.000000000000000000, -1.000000000000000000 ) ) ;
#5470=EDGE_CURVE ( 'NONE', #11540, #14941, #11983, .T. ) ;
#5491=ADVANCED_FACE ( 'NONE', ( #6461 ), #16943, .F. ) ;
#5497=STYLED_ITEM ( 'NONE', ( #6245 ), #3244 ) ;
#5549=VECTOR ( 'NONE', #14749, 1000.000000000000000 ) ;
#5562=LINE ( 'NONE', #169, #4698 ) ;
#5580=DIRECTION ( 'NONE',  ( -1.000000000000000000, -0.000000000000000000, -0.000000000000000000 ) ) ;
#5589=ORIENTED_EDGE ( 'NONE', *, *, #3322, .T. ) ;
#5596=ORIENTED_EDGE ( 'NONE', *, *, #14460, .T. ) ;
#5623=DIRECTION ( 'NONE',  ( -0.000000000000000000, -1.000000000000000000, -0.000000000000000000 ) ) ;
#5632=EDGE_CURVE ( 'NONE', #9647, #6048, #10996, .T. ) ;
#5639=ORIENTED_EDGE ( 'NONE', *, *, #8143, .T. ) ;
#5663=CARTESIAN_POINT ( 'NONE',  ( -31.00000000000002842, 0.000000000000000000, 31.00000000000000000 ) ) ;
#5672=AXIS2_PLACEMENT_3D ( 'NONE', #6534, #9304, #13090 ) ;
#5707=CYLINDRICAL_SURFACE ( 'NONE', #15961, 36.50000000000000000 ) ;
#5716=PLANE ( 'NONE',  #12693 ) ;
#5732=ORIENTED_EDGE ( 'NONE', *, *, #12358, .T. ) ;
#5747=EDGE_LOOP ( 'NONE', ( #6720, #16694, #13814, #2733 ) ) ;
#5768=CARTESIAN_POINT ( 'NONE',  ( -21.00000000000002842, -20.00000000000000000, -37.50000000000000000 ) ) ;
#5769=VECTOR ( 'NONE', #2353, 1000.000000000000000 ) ;
#5793=VECTOR ( 'NONE', #13951, 1000.000000000000000 ) ;
#5801=EDGE_LOOP ( 'NONE', ( #8599, #1067, #9097, #9210 ) ) ;
#5802=EDGE_LOOP ( 'NONE', ( #12344, #2134, #3224, #7597 ) ) ;
#5819=DIRECTION ( 'NONE',  ( 0.000000000000000000, 0.000000000000000000, 1.000000000000000000 ) ) ;
#5857=CARTESIAN_POINT ( 'NONE',  ( -20.00000000000003197, 0.000000000000000000, 40.00000000000000711 ) ) ;
#5862=CARTESIAN_POINT ( 'NONE',  ( 35.00000000000003553, 3.000000000000000000, -20.99999999999999645 ) ) ;
#5865=VERTEX_POINT ( 'NONE', #606 ) ;
#5875=PLANE ( 'NONE',  #2508 ) ;
#5897=CARTESIAN_POINT ( 'NONE',  ( 30.99999999999999645, 3.000000000000000000, -25.99999999999999645 ) ) ;
#5900=CARTESIAN_POINT ( 'NONE',  ( -31.00000000000006395, 3.000000000000000000, -25.99999999999999645 ) ) ;
#5917=VERTEX_POINT ( 'NONE', #15536 ) ;
#5918=DIRECTION ( 'NONE',  ( 0.000000000000000000, -1.000000000000000000, 0.000000000000000000 ) ) ;
#5927=DIRECTION ( 'NONE',  ( 0.000000000000000000, 0.000000000000000000, -1.000000000000000000 ) ) ;
#5928=VERTEX_POINT ( 'NONE', #3687 ) ;
#5938=CIRCLE ( 'NONE', #8959, 2.500000000000002220 ) ;
#5940=LINE ( 'NONE', #7215, #9931 ) ;
#5944=CYLINDRICAL_SURFACE ( 'NONE', #7012, 2.500000000000002220 ) ;
#5950=AXIS2_PLACEMENT_3D ( 'NONE', #12731, #9988, #8779 ) ;
#5957=DIRECTION ( 'NONE',  ( -0.000000000000000000, 1.000000000000000000, -0.000000000000000000 ) ) ;
#5991=FACE_BOUND ( 'NONE', #8475, .T. ) ;
#5996=CARTESIAN_POINT ( 'NONE',  ( 30.99999999999995737, 3.000000000000000000, 31.00000000000000000 ) ) ;
#6034=DIRECTION ( 'NONE',  ( 1.000000000000000000, -0.000000000000000000, 0.000000000000000000 ) ) ;
#6048=VERTEX_POINT ( 'NONE', #1533 ) ;
#6049=DIRECTION ( 'NONE',  ( 0.000000000000000000, 1.000000000000000000, 0.000000000000000000 ) ) ;
#6068=AXIS2_PLACEMENT_3D ( 'NONE', #7878, #13133, #1360 ) ;
#6069=ORIENTED_EDGE ( 'NONE', *, *, #3216, .T. ) ;
#6071=ORIENTED_EDGE ( 'NONE', *, *, #1524, .F. ) ;
#6073=EDGE_CURVE ( 'NONE', #13726, #2088, #8309, .T. ) ;
#6076=DIRECTION ( 'NONE',  ( -0.000000000000000000, 1.000000000000000000, -0.000000000000000000 ) ) ;
#6083=DIRECTION ( 'NONE',  ( -0.000000000000000000, -0.000000000000000000, 1.000000000000000000 ) ) ;
#6100=AXIS2_PLACEMENT_3D ( 'NONE', #7784, #6316, #2465 ) ;
#6134=AXIS2_PLACEMENT_3D ( 'NONE', #8033, #6743, #16031 ) ;
#6206=CARTESIAN_POINT ( 'NONE',  ( 0.000000000000000000, 50.00000000000000000, 0.000000000000000000 ) ) ;
#6224=DIRECTION ( 'NONE',  ( -0.000000000000000000, -1.000000000000000000, 0.000000000000000000 ) ) ;
#6234=EDGE_CURVE ( 'NONE', #1137, #3021, #12526, .T. ) ;
#6245=PRESENTATION_STYLE_ASSIGNMENT (( #12798 ) ) ;
#6253=AXIS2_PLACEMENT_3D ( 'NONE', #8931, #14169, #7620 ) ;
#6260=CARTESIAN_POINT ( 'NONE',  ( -26.00000000000002842, 3.000000000000000000, -31.00000000000003197 ) ) ;
#6282=LINE ( 'NONE', #3813, #13796 ) ;
#6316=DIRECTION ( 'NONE',  ( 0.000000000000000000, 1.000000000000000000, 0.000000000000000000 ) ) ;
#6323=ORIENTED_EDGE ( 'NONE', *, *, #3297, .F. ) ;
#6330=ADVANCED_FACE ( 'NONE', ( #3582 ), #2608, .F. ) ;
#6332=VERTEX_POINT ( 'NONE', #11470 ) ;
#6334=ADVANCED_FACE ( 'NONE', ( #6717 ), #123, .F. ) ;
#6344=FACE_OUTER_BOUND ( 'NONE', #1454, .T. ) ;
#6373=ORIENTED_EDGE ( 'NONE', *, *, #11255, .F. ) ;
#6377=AXIS2_PLACEMENT_3D ( 'NONE', #15242, #1925, #7406 ) ;
#6388=VECTOR ( 'NONE', #13263, 1000.000000000000000 ) ;
#6395=EDGE_CURVE ( 'NONE', #9705, #6745, #10592, .T. ) ;
#6407=DIRECTION ( 'NONE',  ( 0.000000000000000000, 0.000000000000000000, -1.000000000000000000 ) ) ;
#6420=FACE_OUTER_BOUND ( 'NONE', #15797, .T. ) ;
#6431=DIRECTION ( 'NONE',  ( 0.000000000000000000, 0.000000000000000000, 1.000000000000000000 ) ) ;
#6433=EDGE_LOOP ( 'NONE', ( #3638, #7524 ) ) ;
#6461=FACE_OUTER_BOUND ( 'NONE', #864, .T. ) ;
#6462=EDGE_CURVE ( 'NONE', #10795, #7998, #5938, .T. ) ;
#6483=AXIS2_PLACEMENT_3D ( 'NONE', #1469, #2490, #7897 ) ;
#6508=DIRECTION ( 'NONE',  ( 1.000000000000000000, 0.000000000000000000, 0.000000000000000000 ) ) ;
#6511=ORIENTED_EDGE ( 'NONE', *, *, #16716, .F. ) ;
#6512=DIRECTION ( 'NONE',  ( 0.000000000000000000, 0.000000000000000000, -1.000000000000000000 ) ) ;
#6522=ORIENTED_EDGE ( 'NONE', *, *, #13839, .T. ) ;
#6534=CARTESIAN_POINT ( 'NONE',  ( 40.00000000000003553, 3.000000000000000000, 26.00000000000000355 ) ) ;
#6539=DIRECTION ( 'NONE',  ( -0.000000000000000000, -1.000000000000000000, -0.000000000000000000 ) ) ;
#6552=LINE ( 'NONE', #144, #3355 ) ;
#6573=ORIENTED_EDGE ( 'NONE', *, *, #1266, .F. ) ;
#6581=( NAMED_UNIT ( * ) SI_UNIT ( $, .STERADIAN. ) SOLID_ANGLE_UNIT ( ) );
#6594=ORIENTED_EDGE ( 'NONE', *, *, #42, .T. ) ;
#6595=CARTESIAN_POINT ( 'NONE',  ( -26.00000000000002842, 3.000000000000000000, 34.00000000000000711 ) ) ;
#6602=DIRECTION ( 'NONE',  ( 0.000000000000000000, 0.000000000000000000, 1.000000000000000000 ) ) ;
#6614=CARTESIAN_POINT ( 'NONE',  ( -31.00000000000006750, 0.000000000000000000, 26.00000000000000355 ) ) ;
#6646=LINE ( 'NONE', #9330, #5549 ) ;
#6664=EDGE_CURVE ( 'NONE', #13185, #5045, #7865, .T. ) ;
#6681=CARTESIAN_POINT ( 'NONE',  ( -33.99999999999997158, 0.000000000000000000, 31.00000000000000000 ) ) ;
#6688=DIRECTION ( 'NONE',  ( 0.000000000000000000, 0.000000000000000000, 1.000000000000000000 ) ) ;
#6701=VECTOR ( 'NONE', #2196, 1000.000000000000000 ) ;
#6704=EDGE_LOOP ( 'NONE', ( #3469, #6798, #3354, #2011, #8197, #16598, #9567, #217, #3187, #9397, #11878, #7915, #14610, #10500, #8439, #14064, #6573, #2904, #7228, #16325, #7473, #14081, #16069, #13706, #11699, #16353, #13444, #6511 ) ) ;
#6717=FACE_OUTER_BOUND ( 'NONE', #13354, .T. ) ;
#6720=ORIENTED_EDGE ( 'NONE', *, *, #7546, .T. ) ;
#6733=ORIENTED_EDGE ( 'NONE', *, *, #6234, .F. ) ;
#6734=ADVANCED_FACE ( 'NONE', ( #721 ), #5944, .F. ) ;
#6743=DIRECTION ( 'NONE',  ( 1.000000000000000000, 0.000000000000000000, 0.000000000000000000 ) ) ;
#6745=VERTEX_POINT ( 'NONE', #3793 ) ;
#6746=LINE ( 'NONE', #4017, #436 ) ;
#6754=ADVANCED_FACE ( 'NONE', ( #3713 ), #10, .F. ) ;
#6767=CARTESIAN_POINT ( 'NONE',  ( -26.00000000000002842, 3.000000000000000000, 34.00000000000000711 ) ) ;
#6786=ORIENTED_EDGE ( 'NONE', *, *, #4790, .F. ) ;
#6798=ORIENTED_EDGE ( 'NONE', *, *, #3147, .F. ) ;
#6799=DIRECTION ( 'NONE',  ( -1.000000000000000000, 0.000000000000000000, -0.000000000000000000 ) ) ;
#6800=ORIENTED_EDGE ( 'NONE', *, *, #5035, .F. ) ;
#6801=DIRECTION ( 'NONE',  ( -1.000000000000000000, 0.000000000000000000, 0.000000000000000000 ) ) ;
#6815=CARTESIAN_POINT ( 'NONE',  ( -39.99999999999997868, 3.000000000000000000, 26.00000000000000355 ) ) ;
#6818=LINE ( 'NONE', #16189, #13424 ) ;
#6821=PLANE ( 'NONE',  #6134 ) ;
#6822=DIRECTION ( 'NONE',  ( 0.000000000000000000, 0.000000000000000000, -1.000000000000000000 ) ) ;
#6825=CARTESIAN_POINT ( 'NONE',  ( 30.99999999999995737, 0.000000000000000000, 31.00000000000000000 ) ) ;
#6828=CARTESIAN_POINT ( 'NONE',  ( -21.00000000000002842, 3.000000000000000000, -37.50000000000000000 ) ) ;
#6830=ADVANCED_FACE ( 'NONE', ( #6344 ), #11770, .F. ) ;
#6841=CARTESIAN_POINT ( 'NONE',  ( -21.00000000000002842, 3.000000000000000000, -34.99999999999999289 ) ) ;
#6881=ORIENTED_EDGE ( 'NONE', *, *, #2362, .F. ) ;
#6882=VERTEX_POINT ( 'NONE', #4219 ) ;
#6907=AXIS2_PLACEMENT_3D ( 'NONE', #3749, #8985, #16697 ) ;
#6913=ORIENTED_EDGE ( 'NONE', *, *, #15195, .T. ) ;
#6923=AXIS2_PLACEMENT_3D ( 'NONE', #8500, #5918, #9797 ) ;
#6956=ORIENTED_EDGE ( 'NONE', *, *, #4280, .F. ) ;
#6959=CARTESIAN_POINT ( 'NONE',  ( -26.00000000000002842, 3.000000000000000000, -39.99999999999999289 ) ) ;
#6963=AXIS2_PLACEMENT_3D ( 'NONE', #14831, #1862, #15075 ) ;
#6965=VECTOR ( 'NONE', #6076, 1000.000000000000000 ) ;
#6972=VECTOR ( 'NONE', #12727, 1000.000000000000000 ) ;
#7000=EDGE_CURVE ( 'NONE', #11956, #8711, #15366, .T. ) ;
#7007=PLANE ( 'NONE',  #11943 ) ;
#7012=AXIS2_PLACEMENT_3D ( 'NONE', #4642, #7812, #2665 ) ;
#7020=CARTESIAN_POINT ( 'NONE',  ( 30.99999999999999645, 3.000000000000000000, -25.99999999999999645 ) ) ;
#7028=FACE_BOUND ( 'NONE', #15045, .T. ) ;
#7038=DIRECTION ( 'NONE',  ( -0.000000000000000000, -1.000000000000000000, -0.000000000000000000 ) ) ;
#7080=ORIENTED_EDGE ( 'NONE', *, *, #8262, .F. ) ;
#7130=AXIS2_PLACEMENT_3D ( 'NONE', #819, #16188, #8541 ) ;
#7134=COLOUR_RGB ( '', 0.66274510, 0.83137255, 0.94901961) ;
#7142=ORIENTED_EDGE ( 'NONE', *, *, #2362, .T. ) ;
#7170=ORIENTED_EDGE ( 'NONE', *, *, #3346, .T. ) ;
#7187=CARTESIAN_POINT ( 'NONE',  ( 30.99999999999999645, 3.000000000000000000, 26.00000000000000355 ) ) ;
#7196=CARTESIAN_POINT ( 'NONE',  ( 4.163799117101000559E-15, 0.000000000000000000, 34.00000000000000000 ) ) ;
#7212=AXIS2_PLACEMENT_3D ( 'NONE', #4934, #14052, #7760 ) ;
#7215=CARTESIAN_POINT ( 'NONE',  ( -39.99999999999997868, 0.000000000000000000, 26.00000000000000355 ) ) ;
#7228=ORIENTED_EDGE ( 'NONE', *, *, #12914, .F. ) ;
#7256=PLANE ( 'NONE',  #3869 ) ;
#7282=EDGE_CURVE ( 'NONE', #11595, #3880, #1537, .T. ) ;
#7304=EDGE_CURVE ( 'NONE', #175, #6882, #3079, .T. ) ;
#7308=LINE ( 'NONE', #5857, #3952 ) ;
#7321=DIRECTION ( 'NONE',  ( 0.000000000000000000, 0.000000000000000000, -1.000000000000000000 ) ) ;
#7328=CARTESIAN_POINT ( 'NONE',  ( 0.000000000000000000, 50.00000000000000000, 0.000000000000000000 ) ) ;
#7329=DIRECTION ( 'NONE',  ( -0.000000000000000000, 1.000000000000000000, -0.000000000000000000 ) ) ;
#7341=VERTEX_POINT ( 'NONE', #15952 ) ;
#7342=EDGE_CURVE ( 'NONE', #16466, #5917, #9244, .T. ) ;
#7349=DIRECTION ( 'NONE',  ( 0.000000000000000000, -1.000000000000000000, 0.000000000000000000 ) ) ;
#7406=DIRECTION ( 'NONE',  ( 0.000000000000000000, 0.000000000000000000, 1.000000000000000000 ) ) ;
#7446=ORIENTED_EDGE ( 'NONE', *, *, #3086, .T. ) ;
#7459=CIRCLE ( 'NONE', #13797, 2.500000000000002220 ) ;
#7461=LINE ( 'NONE', #16826, #6972 ) ;
#7463=CARTESIAN_POINT ( 'NONE',  ( 30.99999999999999645, 3.000000000000000000, 26.00000000000000355 ) ) ;
#7473=ORIENTED_EDGE ( 'NONE', *, *, #5632, .F. ) ;
#7481=VECTOR ( 'NONE', #15325, 1000.000000000000000 ) ;
#7482=CARTESIAN_POINT ( 'NONE',  ( 4.163799117101000559E-15, 16.00000000000000000, 34.00000000000000000 ) ) ;
#7499=ORIENTED_EDGE ( 'NONE', *, *, #16422, .F. ) ;
#7507=FACE_OUTER_BOUND ( 'NONE', #994, .T. ) ;
#7524=ORIENTED_EDGE ( 'NONE', *, *, #6462, .F. ) ;
#7532=CARTESIAN_POINT ( 'NONE',  ( -34.99999999999998579, 0.000000000000000000, 21.00000000000000355 ) ) ;
#7534=ORIENTED_EDGE ( 'NONE', *, *, #12840, .T. ) ;
#7546=EDGE_CURVE ( 'NONE', #6048, #3292, #9162, .T. ) ;
#7547=ORIENTED_EDGE ( 'NONE', *, *, #8546, .T. ) ;
#7591=DIRECTION ( 'NONE',  ( 0.000000000000000000, -1.000000000000000000, 0.000000000000000000 ) ) ;
#7597=ORIENTED_EDGE ( 'NONE', *, *, #2867, .T. ) ;
#7620=DIRECTION ( 'NONE',  ( 0.000000000000000000, 0.000000000000000000, 1.000000000000000000 ) ) ;
#7628=AXIS2_PLACEMENT_3D ( 'NONE', #5996, #3101, #6407 ) ;
#7661=CARTESIAN_POINT ( 'NONE',  ( 25.99999999999996092, 0.000000000000000000, -33.99999999999998579 ) ) ;
#7684=ORIENTED_EDGE ( 'NONE', *, *, #14985, .T. ) ;
#7719=CIRCLE ( 'NONE', #622, 2.500000000000002220 ) ;
#7720=AXIS2_PLACEMENT_3D ( 'NONE', #1370, #13228, #4038 ) ;
#7736=CARTESIAN_POINT ( 'NONE',  ( 4.469960816887838430E-15, 3.000000000000000000, 36.50000000000000000 ) ) ;
#7745=CARTESIAN_POINT ( 'NONE',  ( -20.00000000000003197, 0.000000000000000000, 37.00000000000000711 ) ) ;
#7756=FACE_BOUND ( 'NONE', #16245, .T. ) ;
#7760=DIRECTION ( 'NONE',  ( 0.000000000000000000, 0.000000000000000000, 1.000000000000000000 ) ) ;
#7762=CARTESIAN_POINT ( 'NONE',  ( -31.00000000000003197, 3.000000000000000000, -30.99999999999999289 ) ) ;
#7766=CARTESIAN_POINT ( 'NONE',  ( -26.00000000000002842, 0.000000000000000000, -31.00000000000003197 ) ) ;
#7774=LINE ( 'NONE', #5122, #15228 ) ;
#7784=CARTESIAN_POINT ( 'NONE',  ( 37.00000000000003553, 3.000000000000000000, 23.00000000000000355 ) ) ;
#7791=SURFACE_STYLE_FILL_AREA ( #2564 ) ;
#7794=ORIENTED_EDGE ( 'NONE', *, *, #7000, .F. ) ;
#7806=EDGE_CURVE ( 'NONE', #6882, #1506, #13633, .T. ) ;
#7812=DIRECTION ( 'NONE',  ( -0.000000000000000000, 1.000000000000000000, -0.000000000000000000 ) ) ;
#7815=DIRECTION ( 'NONE',  ( -0.000000000000000000, 1.000000000000000000, -0.000000000000000000 ) ) ;
#7818=CARTESIAN_POINT ( 'NONE',  ( -20.00000000000003197, 0.000000000000000000, 37.00000000000000711 ) ) ;
#7833=DIRECTION ( 'NONE',  ( -0.000000000000000000, -1.000000000000000000, -0.000000000000000000 ) ) ;
#7844=DIRECTION ( 'NONE',  ( 0.000000000000000000, -0.000000000000000000, 1.000000000000000000 ) ) ;
#7846=ORIENTED_EDGE ( 'NONE', *, *, #5298, .F. ) ;
#7854=DIRECTION ( 'NONE',  ( 0.000000000000000000, 0.000000000000000000, 1.000000000000000000 ) ) ;
#7858=DIRECTION ( 'NONE',  ( 0.000000000000000000, 0.000000000000000000, -1.000000000000000000 ) ) ;
#7859=CARTESIAN_POINT ( 'NONE',  ( 30.99999999999999645, 0.000000000000000000, 26.00000000000000355 ) ) ;
#7864=CARTESIAN_POINT ( 'NONE',  ( 35.00000000000003553, 3.000000000000000000, -23.50000000000000000 ) ) ;
#7865=CIRCLE ( 'NONE', #5950, 3.000000000000002665 ) ;
#7878=CARTESIAN_POINT ( 'NONE',  ( -31.00000000000003197, 3.000000000000000000, -30.99999999999999289 ) ) ;
#7881=CARTESIAN_POINT ( 'NONE',  ( 35.00000000000003553, 3.000000000000000000, -18.49999999999999645 ) ) ;
#7894=ORIENTED_EDGE ( 'NONE', *, *, #8262, .T. ) ;
#7897=DIRECTION ( 'NONE',  ( 0.000000000000000000, 0.000000000000000000, 1.000000000000000000 ) ) ;
#7905=ORIENTED_EDGE ( 'NONE', *, *, #15287, .F. ) ;
#7915=ORIENTED_EDGE ( 'NONE', *, *, #13616, .F. ) ;
#7921=CARTESIAN_POINT ( 'NONE',  ( -31.00000000000006750, 3.000000000000000000, 26.00000000000000355 ) ) ;
#7928=LINE ( 'NONE', #9398, #13620 ) ;
#7935=ORIENTED_EDGE ( 'NONE', *, *, #13839, .F. ) ;
#7947=VERTEX_POINT ( 'NONE', #7745 ) ;
#7949=DIRECTION ( 'NONE',  ( -0.000000000000000000, -1.000000000000000000, 0.000000000000000000 ) ) ;
#7953=DIRECTION ( 'NONE',  ( -0.000000000000000000, 1.000000000000000000, -0.000000000000000000 ) ) ;
#7963=VERTEX_POINT ( 'NONE', #8974 ) ;
#7970=MECHANICAL_DESIGN_GEOMETRIC_PRESENTATION_REPRESENTATION('',(#5497),#15944);
#7979=CARTESIAN_POINT ( 'NONE',  ( -23.00000000000003197, 3.000000000000000000, 37.00000000000000711 ) ) ;
#7990=ORIENTED_EDGE ( 'NONE', *, *, #14774, .F. ) ;
#7998=VERTEX_POINT ( 'NONE', #9050 ) ;
#8000=DIRECTION ( 'NONE',  ( 0.000000000000000000, 0.000000000000000000, 1.000000000000000000 ) ) ;
#8007=VERTEX_POINT ( 'NONE', #14210 ) ;
#8008=CIRCLE ( 'NONE', #12969, 2.500000000000002220 ) ;
#8010=CIRCLE ( 'NONE', #4990, 34.00000000000000000 ) ;
#8017=CIRCLE ( 'NONE', #12155, 2.500000000000002220 ) ;
#8033=CARTESIAN_POINT ( 'NONE',  ( -33.99999999999997158, -20.00000000000000000, -22.99999999999999645 ) ) ;
#8044=FACE_OUTER_BOUND ( 'NONE', #9036, .T. ) ;
#8090=PRODUCT_DEFINITION_SHAPE ( 'NONE', 'NONE',  #13469 ) ;
#8095=CARTESIAN_POINT ( 'NONE',  ( -39.99999999999997868, 3.000000000000000000, 26.00000000000000355 ) ) ;
#8127=FACE_OUTER_BOUND ( 'NONE', #11291, .T. ) ;
#8143=EDGE_CURVE ( 'NONE', #14371, #13400, #15833, .T. ) ;
#8148=ORIENTED_EDGE ( 'NONE', *, *, #897, .T. ) ;
#8150=DIRECTION ( 'NONE',  ( -0.000000000000000000, -1.000000000000000000, 0.000000000000000000 ) ) ;
#8158=ADVANCED_FACE ( 'NONE', ( #1583 ), #15744, .F. ) ;
#8173=CARTESIAN_POINT ( 'NONE',  ( -36.99999999999997868, 0.000000000000000000, -19.99999999999999289 ) ) ;
#8196=ORIENTED_EDGE ( 'NONE', *, *, #10341, .F. ) ;
#8197=ORIENTED_EDGE ( 'NONE', *, *, #4973, .F. ) ;
#8198=DIRECTION ( 'NONE',  ( 0.000000000000000000, -0.000000000000000000, -1.000000000000000000 ) ) ;
#8214=EDGE_CURVE ( 'NONE', #11589, #15821, #5433, .T. ) ;
#8217=VERTEX_POINT ( 'NONE', #1664 ) ;
#8248=CARTESIAN_POINT ( 'NONE',  ( 37.00000000000003553, -20.00000000000000000, 20.00000000000000000 ) ) ;
#8256=ORIENTED_EDGE ( 'NONE', *, *, #13911, .F. ) ;
#8262=EDGE_CURVE ( 'NONE', #12261, #10598, #3134, .T. ) ;
#8296=ORIENTED_EDGE ( 'NONE', *, *, #14431, .T. ) ;
#8309=LINE ( 'NONE', #12011, #8418 ) ;
#8329=CIRCLE ( 'NONE', #929, 4.999999999999997335 ) ;
#8418=VECTOR ( 'NONE', #4105, 1000.000000000000000 ) ;
#8427=DIRECTION ( 'NONE',  ( -0.000000000000000000, -1.000000000000000000, -0.000000000000000000 ) ) ;
#8439=ORIENTED_EDGE ( 'NONE', *, *, #8546, .F. ) ;
#8445=DIRECTION ( 'NONE',  ( 0.000000000000000000, 0.000000000000000000, -1.000000000000000000 ) ) ;
#8475=EDGE_LOOP ( 'NONE', ( #16138, #16326 ) ) ;
#8479=CARTESIAN_POINT ( 'NONE',  ( 19.99999999999995381, 0.000000000000000000, -39.99999999999999289 ) ) ;
#8490=CIRCLE ( 'NONE', #7130, 36.50000000000000000 ) ;
#8500=CARTESIAN_POINT ( 'NONE',  ( 30.99999999999995737, 0.000000000000000000, 31.00000000000000000 ) ) ;
#8515=DIRECTION ( 'NONE',  ( -0.000000000000000000, -1.000000000000000000, -0.000000000000000000 ) ) ;
#8521=VECTOR ( 'NONE', #16608, 1000.000000000000000 ) ;
#8522=DIRECTION ( 'NONE',  ( 1.000000000000000000, 0.000000000000000000, 0.000000000000000000 ) ) ;
#8541=DIRECTION ( 'NONE',  ( 0.000000000000000000, 0.000000000000000000, 1.000000000000000000 ) ) ;
#8544=DIRECTION ( 'NONE',  ( -1.000000000000000000, -0.000000000000000000, -0.000000000000000000 ) ) ;
#8546=EDGE_CURVE ( 'NONE', #4127, #5865, #3336, .T. ) ;
#8554=ORIENTED_EDGE ( 'NONE', *, *, #2225, .F. ) ;
#8564=CARTESIAN_POINT ( 'NONE',  ( 25.99999999999996092, 3.000000000000000000, -31.00000000000003197 ) ) ;
#8597=CARTESIAN_POINT ( 'NONE',  ( -26.00000000000002842, 3.000000000000000000, 31.00000000000003908 ) ) ;
#8599=ORIENTED_EDGE ( 'NONE', *, *, #10862, .T. ) ;
#8604=( NAMED_UNIT ( * ) SI_UNIT ( $, .STERADIAN. ) SOLID_ANGLE_UNIT ( ) );
#8605=VECTOR ( 'NONE', #11297, 1000.000000000000000 ) ;
#8608=FACE_OUTER_BOUND ( 'NONE', #5259, .T. ) ;
#8631=CARTESIAN_POINT ( 'NONE',  ( -39.99999999999997868, 3.000000000000000000, 26.00000000000000355 ) ) ;
#8638=DIRECTION ( 'NONE',  ( 0.000000000000000000, 1.000000000000000000, 0.000000000000000000 ) ) ;
#8655=DIRECTION ( 'NONE',  ( 0.000000000000000000, 0.000000000000000000, -1.000000000000000000 ) ) ;
#8674=PLANE ( 'NONE',  #6923 ) ;
#8693=DIRECTION ( 'NONE',  ( 0.000000000000000000, 0.000000000000000000, 1.000000000000000000 ) ) ;
#8711=VERTEX_POINT ( 'NONE', #7859 ) ;
#8714=VERTEX_POINT ( 'NONE', #13033 ) ;
#8724=ORIENTED_EDGE ( 'NONE', *, *, #2828, .F. ) ;
#8746=CARTESIAN_POINT ( 'NONE',  ( 31.00000000000001776, 0.000000000000000000, -19.99999999999991473 ) ) ;
#8759=CARTESIAN_POINT ( 'NONE',  ( 25.99999999999996092, 3.000000000000000000, -33.99999999999998579 ) ) ;
#8779=DIRECTION ( 'NONE',  ( 0.000000000000000000, 0.000000000000000000, 1.000000000000000000 ) ) ;
#8808=EDGE_LOOP ( 'NONE', ( #3798, #2350, #2082, #9052 ) ) ;
#8828=VECTOR ( 'NONE', #15871, 1000.000000000000000 ) ;
#8830=CARTESIAN_POINT ( 'NONE',  ( 37.00000000000003553, 3.000000000000000000, 20.00000000000000000 ) ) ;
#8856=FACE_OUTER_BOUND ( 'NONE', #12102, .T. ) ;
#8887=LINE ( 'NONE', #8970, #8521 ) ;
#8904=FACE_BOUND ( 'NONE', #10082, .T. ) ;
#8908=EDGE_LOOP ( 'NONE', ( #13929, #121, #1507, #5589 ) ) ;
#8917=EDGE_CURVE ( 'NONE', #5045, #8217, #9684, .T. ) ;
#8923=CARTESIAN_POINT ( 'NONE',  ( 20.99999999999996092, -20.00000000000000000, 37.50000000000001421 ) ) ;
#8931=CARTESIAN_POINT ( 'NONE',  ( -21.00000000000002842, 3.000000000000000000, -34.99999999999999289 ) ) ;
#8956=PRODUCT_DEFINITION_CONTEXT ( 'detailed design', #2371, 'design' ) ;
#8959=AXIS2_PLACEMENT_3D ( 'NONE', #1906, #12388, #8445 ) ;
#8967=CARTESIAN_POINT ( 'NONE',  ( -39.99999999999997868, 0.000000000000000000, 26.00000000000000355 ) ) ;
#8970=CARTESIAN_POINT ( 'NONE',  ( 19.99999999999995381, 3.000000000000000000, -36.99999999999999289 ) ) ;
#8974=CARTESIAN_POINT ( 'NONE',  ( -33.99999999999997158, 3.000000000000000000, -25.99999999999999645 ) ) ;
#8985=DIRECTION ( 'NONE',  ( 0.000000000000000000, 0.000000000000000000, 1.000000000000000000 ) ) ;
#8997=DIRECTION ( 'NONE',  ( -0.000000000000000000, 1.000000000000000000, -0.000000000000000000 ) ) ;
#9030=DIRECTION ( 'NONE',  ( -0.000000000000000000, -0.000000000000000000, 1.000000000000000000 ) ) ;
#9036=EDGE_LOOP ( 'NONE', ( #7547, #7534, #15937, #9999 ) ) ;
#9037=AXIS2_PLACEMENT_3D ( 'NONE', #12606, #2297, #3844 ) ;
#9049=ORIENTED_EDGE ( 'NONE', *, *, #13377, .T. ) ;
#9050=CARTESIAN_POINT ( 'NONE',  ( 35.00000000000003553, 0.000000000000000000, -18.49999999999999645 ) ) ;
#9052=ORIENTED_EDGE ( 'NONE', *, *, #4280, .T. ) ;
#9054=ORIENTED_EDGE ( 'NONE', *, *, #11715, .T. ) ;
#9060=CARTESIAN_POINT ( 'NONE',  ( 34.00000000000002842, -20.00000000000000000, 26.00000000000000355 ) ) ;
#9088=EDGE_CURVE ( 'NONE', #16656, #14275, #16863, .T. ) ;
#9097=ORIENTED_EDGE ( 'NONE', *, *, #14654, .F. ) ;
#9114=AXIS2_PLACEMENT_3D ( 'NONE', #15662, #7591, #8198 ) ;
#9116=VERTEX_POINT ( 'NONE', #7661 ) ;
#9118=ORIENTED_EDGE ( 'NONE', *, *, #4973, .T. ) ;
#9150=CIRCLE ( 'NONE', #5027, 2.500000000000002220 ) ;
#9160=EDGE_CURVE ( 'NONE', #10672, #11859, #15412, .T. ) ;
#9162=LINE ( 'NONE', #7766, #5108 ) ;
#9178=AXIS2_PLACEMENT_3D ( 'NONE', #12810, #1042, #4975 ) ;
#9191=ORIENTED_EDGE ( 'NONE', *, *, #12914, .T. ) ;
#9193=PRODUCT_DEFINITION_FORMATION_WITH_SPECIFIED_SOURCE ( 'ANY', '', #14966, .NOT_KNOWN. ) ;
#9197=CARTESIAN_POINT ( 'NONE',  ( -20.00000000000003197, 3.000000000000000000, 40.00000000000000711 ) ) ;
#9210=ORIENTED_EDGE ( 'NONE', *, *, #7000, .T. ) ;
#9226=VERTEX_POINT ( 'NONE', #1586 ) ;
#9240=ORIENTED_EDGE ( 'NONE', *, *, #12106, .F. ) ;
#9241=CARTESIAN_POINT ( 'NONE',  ( 4.469960816887838430E-15, 26.00000000000000000, 36.50000000000000000 ) ) ;
#9244=CIRCLE ( 'NONE', #13358, 2.500000000000002220 ) ;
#9257=DIRECTION ( 'NONE',  ( 0.000000000000000000, 0.000000000000000000, -1.000000000000000000 ) ) ;
#9275=AXIS2_PLACEMENT_3D ( 'NONE', #7979, #1559, #12116 ) ;
#9304=DIRECTION ( 'NONE',  ( -1.000000000000000000, 0.000000000000000000, 0.000000000000000000 ) ) ;
#9307=LINE ( 'NONE', #14544, #6388 ) ;
#9309=CARTESIAN_POINT ( 'NONE',  ( 0.000000000000000000, 23.00000000000000000, -34.00000000000000000 ) ) ;
#9325=FACE_OUTER_BOUND ( 'NONE', #13790, .T. ) ;
#9330=CARTESIAN_POINT ( 'NONE',  ( -33.99999999999997158, -20.00000000000000000, -25.99999999999999645 ) ) ;
#9350=DIRECTION ( 'NONE',  ( 0.000000000000000000, 0.000000000000000000, 1.000000000000000000 ) ) ;
#9360=DIRECTION ( 'NONE',  ( -0.000000000000000000, -1.000000000000000000, -0.000000000000000000 ) ) ;
#9377=VECTOR ( 'NONE', #3205, 1000.000000000000000 ) ;
#9383=DIRECTION ( 'NONE',  ( 0.000000000000000000, 0.000000000000000000, 1.000000000000000000 ) ) ;
#9397=ORIENTED_EDGE ( 'NONE', *, *, #897, .F. ) ;
#9398=CARTESIAN_POINT ( 'NONE',  ( 22.99999999999995737, 3.000000000000000000, -33.99999999999998579 ) ) ;
#9400=CIRCLE ( 'NONE', #6100, 3.000000000000002665 ) ;
#9416=DIRECTION ( 'NONE',  ( 0.000000000000000000, 0.000000000000000000, 1.000000000000000000 ) ) ;
#9418=DIRECTION ( 'NONE',  ( 0.000000000000000000, 0.000000000000000000, 1.000000000000000000 ) ) ;
#9422=ORIENTED_EDGE ( 'NONE', *, *, #10248, .F. ) ;
#9426=VECTOR ( 'NONE', #12845, 1000.000000000000000 ) ;
#9442=AXIS2_PLACEMENT_3D ( 'NONE', #14403, #11997, #7858 ) ;
#9454=DIRECTION ( 'NONE',  ( 0.000000000000000000, 0.000000000000000000, -1.000000000000000000 ) ) ;
#9480=DIRECTION ( 'NONE',  ( -0.000000000000000000, -1.000000000000000000, -0.000000000000000000 ) ) ;
#9485=CARTESIAN_POINT ( 'NONE',  ( 34.00000000000002842, -20.00000000000000000, 23.00000000000000355 ) ) ;
#9495=VERTEX_POINT ( 'NONE', #10229 ) ;
#9532=( NAMED_UNIT ( * ) PLANE_ANGLE_UNIT ( ) SI_UNIT ( $, .RADIAN. ) );
#9538=EDGE_CURVE ( 'NONE', #10225, #11540, #15857, .T. ) ;
#9539=DIRECTION ( 'NONE',  ( -1.000000000000000000, -0.000000000000000000, -0.000000000000000000 ) ) ;
#9567=ORIENTED_EDGE ( 'NONE', *, *, #12010, .F. ) ;
#9574=VERTEX_POINT ( 'NONE', #14007 ) ;
#9576=VECTOR ( 'NONE', #9631, 1000.000000000000000 ) ;
#9583=CARTESIAN_POINT ( 'NONE',  ( 37.00000000000003553, 0.000000000000000000, 20.00000000000000000 ) ) ;
#9586=DIRECTION ( 'NONE',  ( 0.000000000000000000, 0.000000000000000000, -1.000000000000000000 ) ) ;
#9595=VECTOR ( 'NONE', #9539, 1000.000000000000000 ) ;
#9631=DIRECTION ( 'NONE',  ( -1.000000000000000000, -0.000000000000000000, -0.000000000000000000 ) ) ;
#9633=VERTEX_POINT ( 'NONE', #6828 ) ;
#9647=VERTEX_POINT ( 'NONE', #8479 ) ;
#9649=LINE ( 'NONE', #5768, #9730 ) ;
#9651=DIRECTION ( 'NONE',  ( 0.000000000000000000, 0.000000000000000000, 1.000000000000000000 ) ) ;
#9668=ORIENTED_EDGE ( 'NONE', *, *, #10607, .F. ) ;
#9684=LINE ( 'NONE', #1604, #4399 ) ;
#9685=ORIENTED_EDGE ( 'NONE', *, *, #7304, .T. ) ;
#9688=CARTESIAN_POINT ( 'NONE',  ( 0.000000000000000000, 50.00000000000000000, 0.000000000000000000 ) ) ;
#9691=VECTOR ( 'NONE', #2648, 1000.000000000000000 ) ;
#9705=VERTEX_POINT ( 'NONE', #10968 ) ;
#9710=CARTESIAN_POINT ( 'NONE',  ( -21.00000000000002842, 0.000000000000000000, -34.99999999999999289 ) ) ;
#9713=ORIENTED_EDGE ( 'NONE', *, *, #2061, .F. ) ;
#9716=FACE_BOUND ( 'NONE', #12918, .T. ) ;
#9727=CIRCLE ( 'NONE', #4507, 3.000000000000002665 ) ;
#9730=VECTOR ( 'NONE', #715, 1000.000000000000000 ) ;
#9736=DIRECTION ( 'NONE',  ( 0.000000000000000000, 0.000000000000000000, -1.000000000000000000 ) ) ;
#9753=ORIENTED_EDGE ( 'NONE', *, *, #7282, .F. ) ;
#9756=ORIENTED_EDGE ( 'NONE', *, *, #6395, .T. ) ;
#9761=LINE ( 'NONE', #562, #15939 ) ;
#9763=DIRECTION ( 'NONE',  ( 0.000000000000000000, 0.000000000000000000, 1.000000000000000000 ) ) ;
#9783=DIRECTION ( 'NONE',  ( 0.000000000000000000, 1.000000000000000000, 0.000000000000000000 ) ) ;
#9784=ORIENTED_EDGE ( 'NONE', *, *, #10985, .T. ) ;
#9797=DIRECTION ( 'NONE',  ( 0.000000000000000000, -0.000000000000000000, -1.000000000000000000 ) ) ;
#9824=ADVANCED_FACE ( 'NONE', ( #15419 ), #7256, .F. ) ;
#9835=DIRECTION ( 'NONE',  ( -1.000000000000000000, 0.000000000000000000, -0.000000000000000000 ) ) ;
#9848=VECTOR ( 'NONE', #3691, 1000.000000000000000 ) ;
#9857=FACE_OUTER_BOUND ( 'NONE', #8808, .T. ) ;
#9873=ORIENTED_EDGE ( 'NONE', *, *, #12459, .F. ) ;
#9874=DIRECTION ( 'NONE',  ( 0.000000000000000000, 1.000000000000000000, 0.000000000000000000 ) ) ;
#9877=ORIENTED_EDGE ( 'NONE', *, *, #14865, .T. ) ;
#9878=CARTESIAN_POINT ( 'NONE',  ( 20.99999999999996092, -20.00000000000000000, 32.50000000000000711 ) ) ;
#9893=LINE ( 'NONE', #4568, #9377 ) ;
#9924=FACE_OUTER_BOUND ( 'NONE', #4576, .T. ) ;
#9926=ORIENTED_EDGE ( 'NONE', *, *, #8917, .T. ) ;
#9927=ORIENTED_EDGE ( 'NONE', *, *, #4142, .F. ) ;
#9931=VECTOR ( 'NONE', #11013, 1000.000000000000000 ) ;
#9964=VECTOR ( 'NONE', #4075, 1000.000000000000000 ) ;
#9977=AXIS2_PLACEMENT_3D ( 'NONE', #12142, #3131, #6799 ) ;
#9988=DIRECTION ( 'NONE',  ( -0.000000000000000000, -1.000000000000000000, -0.000000000000000000 ) ) ;
#9994=ORIENTED_EDGE ( 'NONE', *, *, #3237, .T. ) ;
#9999=ORIENTED_EDGE ( 'NONE', *, *, #11783, .F. ) ;
#10000=CARTESIAN_POINT ( 'NONE',  ( 0.000000000000000000, 26.00000000000000000, 0.000000000000000000 ) ) ;
#10028=ORIENTED_EDGE ( 'NONE', *, *, #12849, .F. ) ;
#10037=EDGE_CURVE ( 'NONE', #14546, #4127, #10186, .T. ) ;
#10045=FACE_OUTER_BOUND ( 'NONE', #6704, .T. ) ;
#10048=LINE ( 'NONE', #9878, #6965 ) ;
#10060=EDGE_CURVE ( 'NONE', #2088, #9116, #9761, .T. ) ;
#10071=ORIENTED_EDGE ( 'NONE', *, *, #10641, .T. ) ;
#10082=EDGE_LOOP ( 'NONE', ( #1725, #8554 ) ) ;
#10149=EDGE_LOOP ( 'NONE', ( #15211, #1225, #13000, #6881 ) ) ;
#10164=LINE ( 'NONE', #2172, #15393 ) ;
#10170=CARTESIAN_POINT ( 'NONE',  ( 0.000000000000000000, 0.000000000000000000, -34.00000000000000000 ) ) ;
#10186=CIRCLE ( 'NONE', #4429, 3.000000000000002665 ) ;
#10188=UNCERTAINTY_MEASURE_WITH_UNIT (LENGTH_MEASURE( 1.000000000000000082E-05 ), #15301, 'distance_accuracy_value', 'NONE');
#10199=CIRCLE ( 'NONE', #2787, 34.00000000000000000 ) ;
#10203=CIRCLE ( 'NONE', #6068, 4.999999999999997335 ) ;
#10205=CARTESIAN_POINT ( 'NONE',  ( -34.99999999999998579, 3.000000000000000000, 18.50000000000000355 ) ) ;
#10216=DIRECTION ( 'NONE',  ( -0.000000000000000000, 1.000000000000000000, -0.000000000000000000 ) ) ;
#10225=VERTEX_POINT ( 'NONE', #4656 ) ;
#10229=CARTESIAN_POINT ( 'NONE',  ( 30.99999999999999645, 3.000000000000000000, -25.99999999999999645 ) ) ;
#10242=CIRCLE ( 'NONE', #7212, 3.000000000000002665 ) ;
#10248=EDGE_CURVE ( 'NONE', #1605, #12055, #11365, .T. ) ;
#10257=CARTESIAN_POINT ( 'NONE',  ( -23.00000000000003197, 0.000000000000000000, 37.00000000000000711 ) ) ;
#10261=VECTOR ( 'NONE', #6602, 1000.000000000000000 ) ;
#10268=CARTESIAN_POINT ( 'NONE',  ( -23.00000000000003197, 3.000000000000000000, 34.00000000000000711 ) ) ;
#10271=EDGE_CURVE ( 'NONE', #1746, #14275, #10164, .T. ) ;
#10276=EDGE_LOOP ( 'NONE', ( #10378, #6323 ) ) ;
#10282=VERTEX_POINT ( 'NONE', #15144 ) ;
#10285=ORIENTED_EDGE ( 'NONE', *, *, #16846, .T. ) ;
#10335=ADVANCED_FACE ( 'NONE', ( #12402 ), #5875, .F. ) ;
#10341=EDGE_CURVE ( 'NONE', #7341, #2045, #12490, .T. ) ;
#10359=CARTESIAN_POINT ( 'NONE',  ( -36.99999999999997868, 0.000000000000000000, -22.99999999999999645 ) ) ;
#10360=CARTESIAN_POINT ( 'NONE',  ( -23.00000000000003197, 3.000000000000000000, 37.00000000000000711 ) ) ;
#10368=DIRECTION ( 'NONE',  ( -0.000000000000000000, -0.000000000000000000, 1.000000000000000000 ) ) ;
#10376=LINE ( 'NONE', #8830, #1425 ) ;
#10378=ORIENTED_EDGE ( 'NONE', *, *, #14431, .F. ) ;
#10393=CARTESIAN_POINT ( 'NONE',  ( 0.000000000000000000, 16.00000000000000000, -34.00000000000000000 ) ) ;
#10426=CARTESIAN_POINT ( 'NONE',  ( 0.000000000000000000, 16.00000000000000000, 0.000000000000000000 ) ) ;
#10441=DIRECTION ( 'NONE',  ( 0.000000000000000000, 0.000000000000000000, -1.000000000000000000 ) ) ;
#10482=CIRCLE ( 'NONE', #7720, 2.500000000000002220 ) ;
#10495=ORIENTED_EDGE ( 'NONE', *, *, #9088, .T. ) ;
#10500=ORIENTED_EDGE ( 'NONE', *, *, #10667, .F. ) ;
#10509=VERTEX_POINT ( 'NONE', #542 ) ;
#10517=LINE ( 'NONE', #9241, #4714 ) ;
#10529=DIRECTION ( 'NONE',  ( 0.000000000000000000, 0.000000000000000000, -1.000000000000000000 ) ) ;
#10533=VECTOR ( 'NONE', #11873, 1000.000000000000000 ) ;
#10535=ORIENTED_EDGE ( 'NONE', *, *, #8917, .F. ) ;
#10543=ADVANCED_FACE ( 'NONE', ( #4140 ), #13254, .F. ) ;
#10569=LINE ( 'NONE', #6595, #2842 ) ;
#10592=LINE ( 'NONE', #14541, #13643 ) ;
#10598=VERTEX_POINT ( 'NONE', #11343 ) ;
#10602=ORIENTED_EDGE ( 'NONE', *, *, #15191, .T. ) ;
#10607=EDGE_CURVE ( 'NONE', #14371, #1759, #10199, .T. ) ;
#10612=AXIS2_PLACEMENT_3D ( 'NONE', #11877, #15828, #8000 ) ;
#10618=DIRECTION ( 'NONE',  ( -1.000000000000000000, 0.000000000000000000, 0.000000000000000000 ) ) ;
#10627=DIRECTION ( 'NONE',  ( 1.000000000000000000, 0.000000000000000000, 1.156482317317870344E-15 ) ) ;
#10637=DIRECTION ( 'NONE',  ( 0.000000000000000000, 0.000000000000000000, -1.000000000000000000 ) ) ;
#10641=EDGE_CURVE ( 'NONE', #11540, #2523, #9893, .T. ) ;
#10643=AXIS2_PLACEMENT_3D ( 'NONE', #8248, #13496, #272 ) ;
#10647=LINE ( 'NONE', #15967, #15964 ) ;
#10662=EDGE_LOOP ( 'NONE', ( #3424, #4911, #10858, #10285 ) ) ;
#10667=EDGE_CURVE ( 'NONE', #5865, #11589, #5940, .T. ) ;
#10672=VERTEX_POINT ( 'NONE', #2072 ) ;
#10686=EDGE_LOOP ( 'NONE', ( #11346, #7935 ) ) ;
#10688=ORIENTED_EDGE ( 'NONE', *, *, #6073, .F. ) ;
#10690=ADVANCED_FACE ( 'NONE', ( #8608 ), #15121, .F. ) ;
#10726=ORIENTED_EDGE ( 'NONE', *, *, #14985, .F. ) ;
#10755=EDGE_LOOP ( 'NONE', ( #7080, #11029, #16347, #13204 ) ) ;
#10779=CARTESIAN_POINT ( 'NONE',  ( -34.99999999999998579, 3.000000000000000000, 23.50000000000000711 ) ) ;
#10785=DIRECTION ( 'NONE',  ( -0.000000000000000000, -1.000000000000000000, 0.000000000000000000 ) ) ;
#10795=VERTEX_POINT ( 'NONE', #11592 ) ;
#10819=VECTOR ( 'NONE', #13152, 1000.000000000000000 ) ;
#10858=ORIENTED_EDGE ( 'NONE', *, *, #12654, .T. ) ;
#10862=EDGE_CURVE ( 'NONE', #8711, #12822, #1290, .T. ) ;
#10878=FACE_OUTER_BOUND ( 'NONE', #16448, .T. ) ;
#10884=DIRECTION ( 'NONE',  ( 0.000000000000000000, -0.000000000000000000, 1.000000000000000000 ) ) ;
#10893=EDGE_CURVE ( 'NONE', #16466, #11217, #10647, .T. ) ;
#10929=ADVANCED_FACE ( 'NONE', ( #16062 ), #4213, .F. ) ;
#10949=DIRECTION ( 'NONE',  ( -0.000000000000000000, -1.000000000000000000, -0.000000000000000000 ) ) ;
#10968=CARTESIAN_POINT ( 'NONE',  ( -31.00000000000006395, 0.000000000000000000, -25.99999999999999645 ) ) ;
#10975=LINE ( 'NONE', #2033, #10976 ) ;
#10976=VECTOR ( 'NONE', #4449, 1000.000000000000000 ) ;
#10985=EDGE_CURVE ( 'NONE', #5033, #1155, #3081, .T. ) ;
#10991=VECTOR ( 'NONE', #11282, 1000.000000000000000 ) ;
#10996=LINE ( 'NONE', #14785, #15793 ) ;
#11013=DIRECTION ( 'NONE',  ( -0.000000000000000000, -0.000000000000000000, 1.000000000000000000 ) ) ;
#11019=DIRECTION ( 'NONE',  ( 0.000000000000000000, 1.000000000000000000, 0.000000000000000000 ) ) ;
#11021=CARTESIAN_POINT ( 'NONE',  ( 35.00000000000003553, -20.00000000000000000, -18.49999999999999645 ) ) ;
#11022=ORIENTED_EDGE ( 'NONE', *, *, #12654, .F. ) ;
#11026=AXIS2_PLACEMENT_3D ( 'NONE', #4296, #8150, #10637 ) ;
#11029=ORIENTED_EDGE ( 'NONE', *, *, #12840, .F. ) ;
#11034=CARTESIAN_POINT ( 'NONE',  ( 20.99999999999996092, 0.000000000000000000, 37.50000000000001421 ) ) ;
#11038=CARTESIAN_POINT ( 'NONE',  ( 20.99999999999996092, -20.00000000000000000, 35.00000000000000711 ) ) ;
#11039=AXIS2_PLACEMENT_3D ( 'NONE', #3958, #3865, #6688 ) ;
#11056=AXIS2_PLACEMENT_3D ( 'NONE', #736, #6034, #1792 ) ;
#11078=ADVANCED_FACE ( 'NONE', ( #5991, #10045, #9716, #522, #7028, #14949 ), #8674, .T. ) ;
#11090=VECTOR ( 'NONE', #7038, 1000.000000000000000 ) ;
#11119=DIRECTION ( 'NONE',  ( 0.000000000000000000, 0.000000000000000000, -1.000000000000000000 ) ) ;
#11128=AXIS2_PLACEMENT_3D ( 'NONE', #827, #6049, #4852 ) ;
#11175=AXIS2_PLACEMENT_3D ( 'NONE', #9485, #6801, #3993 ) ;
#11209=PLANE ( 'NONE',  #6963 ) ;
#11217=VERTEX_POINT ( 'NONE', #12864 ) ;
#11235=LINE ( 'NONE', #7187, #2820 ) ;
#11255=EDGE_CURVE ( 'NONE', #12055, #14343, #9400, .T. ) ;
#11276=CARTESIAN_POINT ( 'NONE',  ( 25.99999999999996092, 0.000000000000000000, 40.00000000000000711 ) ) ;
#11282=DIRECTION ( 'NONE',  ( -0.000000000000000000, -1.000000000000000000, -0.000000000000000000 ) ) ;
#11283=EDGE_CURVE ( 'NONE', #10282, #8714, #8017, .T. ) ;
#11291=EDGE_LOOP ( 'NONE', ( #16158, #13405, #772, #14683 ) ) ;
#11297=DIRECTION ( 'NONE',  ( -1.000000000000000000, -0.000000000000000000, -0.000000000000000000 ) ) ;
#11301=DIRECTION ( 'NONE',  ( 1.000000000000000000, 0.000000000000000000, 0.000000000000000000 ) ) ;
#11307=EDGE_CURVE ( 'NONE', #8714, #10282, #4461, .T. ) ;
#11343=CARTESIAN_POINT ( 'NONE',  ( -39.99999999999997868, 3.000000000000000000, 26.00000000000000355 ) ) ;
#11346=ORIENTED_EDGE ( 'NONE', *, *, #13227, .F. ) ;
#11349=ORIENTED_EDGE ( 'NONE', *, *, #14128, .F. ) ;
#11365=LINE ( 'NONE', #2091, #5793 ) ;
#11369=PLANE ( 'NONE',  #11056 ) ;
#11439=ADVANCED_FACE ( 'NONE', ( #817 ), #1060, .F. ) ;
#11470=CARTESIAN_POINT ( 'NONE',  ( 20.99999999999996092, 0.000000000000000000, 32.50000000000000711 ) ) ;
#11486=ADVANCED_FACE ( 'NONE', ( #3475 ), #11369, .F. ) ;
#11534=ORIENTED_EDGE ( 'NONE', *, *, #14654, .T. ) ;
#11540=VERTEX_POINT ( 'NONE', #12748 ) ;
#11564=AXIS2_PLACEMENT_3D ( 'NONE', #1341, #8997, #3762 ) ;
#11576=ORIENTED_EDGE ( 'NONE', *, *, #1266, .T. ) ;
#11579=VECTOR ( 'NONE', #5105, 1000.000000000000000 ) ;
#11589=VERTEX_POINT ( 'NONE', #8967 ) ;
#11592=CARTESIAN_POINT ( 'NONE',  ( 35.00000000000003553, 0.000000000000000000, -23.50000000000000000 ) ) ;
#11595=VERTEX_POINT ( 'NONE', #5087 ) ;
#11600=FACE_OUTER_BOUND ( 'NONE', #15864, .T. ) ;
#11622=ADVANCED_BREP_SHAPE_REPRESENTATION ( '', ( #3244, #1488 ), #16822 ) ;
#11635=AXIS2_PLACEMENT_3D ( 'NONE', #8095, #15734, #1393 ) ;
#11644=CARTESIAN_POINT ( 'NONE',  ( -26.00000000000002842, 3.000000000000000000, -39.99999999999999289 ) ) ;
#11658=LINE ( 'NONE', #8923, #15701 ) ;
#11669=CARTESIAN_POINT ( 'NONE',  ( 25.99999999999996092, 0.000000000000000000, -31.00000000000003197 ) ) ;
#11696=VERTEX_POINT ( 'NONE', #5000 ) ;
#11699=ORIENTED_EDGE ( 'NONE', *, *, #3237, .F. ) ;
#11715=EDGE_CURVE ( 'NONE', #11859, #7947, #15721, .T. ) ;
#11720=DIRECTION ( 'NONE',  ( 1.000000000000000000, 0.000000000000000000, 0.000000000000000000 ) ) ;
#11731=CARTESIAN_POINT ( 'NONE',  ( -26.00000000000002842, 3.000000000000000000, 34.00000000000000711 ) ) ;
#11752=CARTESIAN_POINT ( 'NONE',  ( 30.99999999999996092, 3.000000000000000000, -30.99999999999999289 ) ) ;
#11755=SURFACE_SIDE_STYLE ('',( #7791 ) ) ;
#11770=CYLINDRICAL_SURFACE ( 'NONE', #754, 34.00000000000000000 ) ;
#11780=ORIENTED_EDGE ( 'NONE', *, *, #1848, .T. ) ;
#11783=EDGE_CURVE ( 'NONE', #4127, #1137, #16165, .T. ) ;
#11798=VECTOR ( 'NONE', #12915, 1000.000000000000000 ) ;
#11806=EDGE_CURVE ( 'NONE', #1759, #14371, #4739, .T. ) ;
#11859=VERTEX_POINT ( 'NONE', #4493 ) ;
#11863=ORIENTED_EDGE ( 'NONE', *, *, #15611, .T. ) ;
#11873=DIRECTION ( 'NONE',  ( 0.000000000000000000, 0.000000000000000000, -1.000000000000000000 ) ) ;
#11877=CARTESIAN_POINT ( 'NONE',  ( -36.99999999999997868, -20.00000000000000000, -22.99999999999999645 ) ) ;
#11878=ORIENTED_EDGE ( 'NONE', *, *, #15780, .F. ) ;
#11884=EDGE_LOOP ( 'NONE', ( #2219, #13501, #14277, #14892 ) ) ;
#11894=ORIENTED_EDGE ( 'NONE', *, *, #13227, .T. ) ;
#11902=DIRECTION ( 'NONE',  ( -0.000000000000000000, 1.000000000000000000, -0.000000000000000000 ) ) ;
#11914=ORIENTED_EDGE ( 'NONE', *, *, #14333, .F. ) ;
#11942=DIRECTION ( 'NONE',  ( 0.000000000000000000, 0.000000000000000000, -1.000000000000000000 ) ) ;
#11943=AXIS2_PLACEMENT_3D ( 'NONE', #9688, #659, #10884 ) ;
#11949=ORIENTED_EDGE ( 'NONE', *, *, #2828, .T. ) ;
#11956=VERTEX_POINT ( 'NONE', #7463 ) ;
#11971=DIRECTION ( 'NONE',  ( -1.000000000000000000, -0.000000000000000000, -0.000000000000000000 ) ) ;
#11972=ORIENTED_EDGE ( 'NONE', *, *, #13593, .T. ) ;
#11974=EDGE_LOOP ( 'NONE', ( #3208, #7142, #2163, #11349 ) ) ;
#11983=LINE ( 'NONE', #1503, #178 ) ;
#11991=AXIS2_PLACEMENT_3D ( 'NONE', #16545, #9783, #16208 ) ;
#11997=DIRECTION ( 'NONE',  ( -0.000000000000000000, -1.000000000000000000, -0.000000000000000000 ) ) ;
#12010=EDGE_CURVE ( 'NONE', #2523, #1746, #7308, .T. ) ;
#12011=CARTESIAN_POINT ( 'NONE',  ( 25.99999999999996092, 3.000000000000000000, -31.00000000000003197 ) ) ;
#12013=LINE ( 'NONE', #16131, #5203 ) ;
#12036=PLANE ( 'NONE',  #10643 ) ;
#12042=ORIENTED_EDGE ( 'NONE', *, *, #485, .T. ) ;
#12055=VERTEX_POINT ( 'NONE', #12813 ) ;
#12065=DIRECTION ( 'NONE',  ( -0.000000000000000000, -1.000000000000000000, -0.000000000000000000 ) ) ;
#12074=LINE ( 'NONE', #6815, #16291 ) ;
#12102=EDGE_LOOP ( 'NONE', ( #10602, #4311, #16206, #14378 ) ) ;
#12106=EDGE_CURVE ( 'NONE', #11696, #12951, #10569, .T. ) ;
#12116=DIRECTION ( 'NONE',  ( 0.000000000000000000, 0.000000000000000000, 1.000000000000000000 ) ) ;
#12119=ADVANCED_FACE ( 'NONE', ( #1295 ), #5068, .F. ) ;
#12123=VERTEX_POINT ( 'NONE', #3966 ) ;
#12142=CARTESIAN_POINT ( 'NONE',  ( -23.00000000000003197, 3.000000000000000000, 34.00000000000000711 ) ) ;
#12155=AXIS2_PLACEMENT_3D ( 'NONE', #7532, #15861, #1613 ) ;
#12215=ORIENTED_EDGE ( 'NONE', *, *, #14774, .T. ) ;
#12235=DIRECTION ( 'NONE',  ( -0.000000000000000000, 1.000000000000000000, -0.000000000000000000 ) ) ;
#12240=CIRCLE ( 'NONE', #11128, 2.500000000000002220 ) ;
#12261=VERTEX_POINT ( 'NONE', #16066 ) ;
#12262=EDGE_LOOP ( 'NONE', ( #9994, #12630, #10688, #7684 ) ) ;
#12272=LINE ( 'NONE', #12431, #3849 ) ;
#12284=VECTOR ( 'NONE', #13442, 1000.000000000000000 ) ;
#12286=CARTESIAN_POINT ( 'NONE',  ( 35.00000000000003553, 3.000000000000000000, -20.99999999999999645 ) ) ;
#12294=ORIENTED_EDGE ( 'NONE', *, *, #13604, .T. ) ;
#12307=AXIS2_PLACEMENT_3D ( 'NONE', #11038, #16110, #9416 ) ;
#12316=SHAPE_REPRESENTATION ( 'Servo-Bas', ( #1488 ), #16822 ) ;
#12321=DIRECTION ( 'NONE',  ( -1.000000000000000000, -0.000000000000000000, -0.000000000000000000 ) ) ;
#12344=ORIENTED_EDGE ( 'NONE', *, *, #13616, .T. ) ;
#12358=EDGE_CURVE ( 'NONE', #6332, #10509, #10048, .T. ) ;
#12380=FACE_OUTER_BOUND ( 'NONE', #15783, .T. ) ;
#12388=DIRECTION ( 'NONE',  ( -0.000000000000000000, -1.000000000000000000, 0.000000000000000000 ) ) ;
#12402=FACE_OUTER_BOUND ( 'NONE', #1647, .T. ) ;
#12404=AXIS2_PLACEMENT_3D ( 'NONE', #13680, #1902, #12472 ) ;
#12406=DIRECTION ( 'NONE',  ( 1.000000000000000000, 0.000000000000000000, -0.000000000000000000 ) ) ;
#12408=LINE ( 'NONE', #648, #10991 ) ;
#12431=CARTESIAN_POINT ( 'NONE',  ( -33.99999999999997158, 3.000000000000000000, -22.99999999999999645 ) ) ;
#12435=AXIS2_PLACEMENT_3D ( 'NONE', #13627, #11902, #5449 ) ;
#12459=EDGE_CURVE ( 'NONE', #9495, #1506, #3188, .T. ) ;
#12472=DIRECTION ( 'NONE',  ( 0.000000000000000000, 0.000000000000000000, 1.000000000000000000 ) ) ;
#12487=FACE_OUTER_BOUND ( 'NONE', #10662, .T. ) ;
#12488=AXIS2_PLACEMENT_3D ( 'NONE', #6825, #7949, #9257 ) ;
#12490=LINE ( 'NONE', #733, #48 ) ;
#12506=FACE_OUTER_BOUND ( 'NONE', #16945, .T. ) ;
#12511=VECTOR ( 'NONE', #512, 1000.000000000000000 ) ;
#12517=CARTESIAN_POINT ( 'NONE',  ( 34.00000000000002842, 0.000000000000000000, 26.00000000000000355 ) ) ;
#12521=DIRECTION ( 'NONE',  ( -1.000000000000000000, 0.000000000000000000, -1.156482317317870344E-15 ) ) ;
#12526=CIRCLE ( 'NONE', #11991, 3.000000000000002665 ) ;
#12533=VECTOR ( 'NONE', #8544, 1000.000000000000000 ) ;
#12569=ORIENTED_EDGE ( 'NONE', *, *, #8214, .T. ) ;
#12598=DIRECTION ( 'NONE',  ( 0.000000000000000000, 0.000000000000000000, -1.000000000000000000 ) ) ;
#12606=CARTESIAN_POINT ( 'NONE',  ( 0.000000000000000000, 3.000000000000000000, 0.000000000000000000 ) ) ;
#12622=ORIENTED_EDGE ( 'NONE', *, *, #14240, .T. ) ;
#12630=ORIENTED_EDGE ( 'NONE', *, *, #10060, .F. ) ;
#12652=DIRECTION ( 'NONE',  ( 0.000000000000000000, 0.000000000000000000, -1.000000000000000000 ) ) ;
#12654=EDGE_CURVE ( 'NONE', #10282, #15314, #12013, .T. ) ;
#12693=AXIS2_PLACEMENT_3D ( 'NONE', #16028, #10618, #1518 ) ;
#12721=( NAMED_UNIT ( * ) PLANE_ANGLE_UNIT ( ) SI_UNIT ( $, .RADIAN. ) );
#12727=DIRECTION ( 'NONE',  ( -0.000000000000000000, 1.000000000000000000, -0.000000000000000000 ) ) ;
#12731=CARTESIAN_POINT ( 'NONE',  ( 22.99999999999995737, 3.000000000000000000, -36.99999999999999289 ) ) ;
#12748=CARTESIAN_POINT ( 'NONE',  ( -20.00000000000003197, 3.000000000000000000, 40.00000000000000711 ) ) ;
#12798=SURFACE_STYLE_USAGE ( .BOTH. , #11755 ) ;
#12802=EDGE_CURVE ( 'NONE', #3021, #7963, #12272, .T. ) ;
#12810=CARTESIAN_POINT ( 'NONE',  ( 22.99999999999995737, 3.000000000000000000, -36.99999999999999289 ) ) ;
#12813=CARTESIAN_POINT ( 'NONE',  ( 37.00000000000003553, 3.000000000000000000, 20.00000000000000000 ) ) ;
#12822=VERTEX_POINT ( 'NONE', #12517 ) ;
#12840=EDGE_CURVE ( 'NONE', #5865, #12261, #10975, .T. ) ;
#12845=DIRECTION ( 'NONE',  ( -0.000000000000000000, -1.000000000000000000, -0.000000000000000000 ) ) ;
#12849=EDGE_CURVE ( 'NONE', #13944, #10509, #16180, .T. ) ;
#12864=CARTESIAN_POINT ( 'NONE',  ( -21.00000000000002842, 3.000000000000000000, -32.49999999999999289 ) ) ;
#12867=EDGE_LOOP ( 'NONE', ( #15976, #7846 ) ) ;
#12869=CARTESIAN_POINT ( 'NONE',  ( -39.99999999999997868, 3.000000000000000000, 26.00000000000000355 ) ) ;
#12882=AXIS2_PLACEMENT_3D ( 'NONE', #4485, #8515, #9736 ) ;
#12891=EDGE_LOOP ( 'NONE', ( #668, #1888, #9240, #7446 ) ) ;
#12893=AXIS2_PLACEMENT_3D ( 'NONE', #13806, #4538, #13892 ) ;
#12896=ORIENTED_EDGE ( 'NONE', *, *, #5298, .T. ) ;
#12908=CARTESIAN_POINT ( 'NONE',  ( -26.00000000000002842, 3.000000000000000000, -31.00000000000003197 ) ) ;
#12914=EDGE_CURVE ( 'NONE', #3292, #9705, #13988, .T. ) ;
#12915=DIRECTION ( 'NONE',  ( -0.000000000000000000, -1.000000000000000000, -0.000000000000000000 ) ) ;
#12916=ORIENTED_EDGE ( 'NONE', *, *, #10893, .F. ) ;
#12918=EDGE_LOOP ( 'NONE', ( #3797, #16597 ) ) ;
#12926=FACE_OUTER_BOUND ( 'NONE', #15901, .T. ) ;
#12951=VERTEX_POINT ( 'NONE', #11731 ) ;
#12969=AXIS2_PLACEMENT_3D ( 'NONE', #6841, #5393, #9350 ) ;
#12982=EDGE_LOOP ( 'NONE', ( #14800, #3529, #942, #11894 ) ) ;
#13000=ORIENTED_EDGE ( 'NONE', *, *, #11255, .T. ) ;
#13019=FACE_OUTER_BOUND ( 'NONE', #1162, .T. ) ;
#13030=CARTESIAN_POINT ( 'NONE',  ( 35.00000000000003553, 0.000000000000000000, -20.99999999999999645 ) ) ;
#13033=CARTESIAN_POINT ( 'NONE',  ( -34.99999999999998579, 0.000000000000000000, 18.50000000000000355 ) ) ;
#13052=LINE ( 'NONE', #14174, #5195 ) ;
#13090=DIRECTION ( 'NONE',  ( 0.000000000000000000, 0.000000000000000000, 1.000000000000000000 ) ) ;
#13092=LINE ( 'NONE', #12908, #1736 ) ;
#13095=DIRECTION ( 'NONE',  ( 1.000000000000000000, -0.000000000000000000, -0.000000000000000000 ) ) ;
#13131=ADVANCED_FACE ( 'NONE', ( #1338 ), #5271, .F. ) ;
#13133=DIRECTION ( 'NONE',  ( -0.000000000000000000, -1.000000000000000000, 0.000000000000000000 ) ) ;
#13149=CARTESIAN_POINT ( 'NONE',  ( 0.000000000000000000, 23.00000000000000000, 0.000000000000000000 ) ) ;
#13152=DIRECTION ( 'NONE',  ( -0.000000000000000000, 1.000000000000000000, -0.000000000000000000 ) ) ;
#13176=ORIENTED_EDGE ( 'NONE', *, *, #879, .F. ) ;
#13185=VERTEX_POINT ( 'NONE', #2969 ) ;
#13194=EDGE_CURVE ( 'NONE', #11595, #5928, #14513, .T. ) ;
#13204=ORIENTED_EDGE ( 'NONE', *, *, #16683, .F. ) ;
#13216=DIRECTION ( 'NONE',  ( -0.000000000000000000, -1.000000000000000000, 0.000000000000000000 ) ) ;
#13227=EDGE_CURVE ( 'NONE', #3880, #15603, #8490, .T. ) ;
#13228=DIRECTION ( 'NONE',  ( -0.000000000000000000, -1.000000000000000000, 0.000000000000000000 ) ) ;
#13237=AXIS2_PLACEMENT_3D ( 'NONE', #4510, #10949, #14900 ) ;
#13252=ORIENTED_EDGE ( 'NONE', *, *, #15287, .T. ) ;
#13254=PLANE ( 'NONE',  #4704 ) ;
#13263=DIRECTION ( 'NONE',  ( 1.000000000000000000, 0.000000000000000000, 1.156482317317870344E-15 ) ) ;
#13286=DIRECTION ( 'NONE',  ( -0.000000000000000000, -1.000000000000000000, -0.000000000000000000 ) ) ;
#13294=FACE_OUTER_BOUND ( 'NONE', #14858, .T. ) ;
#13299=EDGE_CURVE ( 'NONE', #8217, #9647, #12408, .T. ) ;
#13305=DIRECTION ( 'NONE',  ( -0.000000000000000000, -1.000000000000000000, 0.000000000000000000 ) ) ;
#13314=AXIS2_PLACEMENT_3D ( 'NONE', #7020, #5819, #15018 ) ;
#13317=( LENGTH_UNIT ( ) NAMED_UNIT ( * ) SI_UNIT ( .MILLI., .METRE. ) );
#13335=ORIENTED_EDGE ( 'NONE', *, *, #2269, .T. ) ;
#13354=EDGE_LOOP ( 'NONE', ( #1070, #8196, #2411, #853 ) ) ;
#13358=AXIS2_PLACEMENT_3D ( 'NONE', #1700, #13216, #2817 ) ;
#13363=ORIENTED_EDGE ( 'NONE', *, *, #9160, .T. ) ;
#13367=DIRECTION ( 'NONE',  ( -1.000000000000000000, -0.000000000000000000, -0.000000000000000000 ) ) ;
#13377=EDGE_CURVE ( 'NONE', #5045, #12123, #8887, .T. ) ;
#13400=VERTEX_POINT ( 'NONE', #10170 ) ;
#13405=ORIENTED_EDGE ( 'NONE', *, *, #9088, .F. ) ;
#13424=VECTOR ( 'NONE', #7329, 1000.000000000000000 ) ;
#13425=LINE ( 'NONE', #2935, #10819 ) ;
#13433=CARTESIAN_POINT ( 'NONE',  ( 22.99999999999995737, 3.000000000000000000, -33.99999999999998579 ) ) ;
#13442=DIRECTION ( 'NONE',  ( 1.000000000000000000, 0.000000000000000000, 0.000000000000000000 ) ) ;
#13444=ORIENTED_EDGE ( 'NONE', *, *, #7806, .F. ) ;
#13469=PRODUCT_DEFINITION ( 'UNKNOWN', '', #9193, #8956 ) ;
#13488=LINE ( 'NONE', #4115, #14808 ) ;
#13489=DIRECTION ( 'NONE',  ( -0.000000000000000000, -1.000000000000000000, 0.000000000000000000 ) ) ;
#13496=DIRECTION ( 'NONE',  ( 1.156482317317870344E-15, 0.000000000000000000, -1.000000000000000000 ) ) ;
#13501=ORIENTED_EDGE ( 'NONE', *, *, #11783, .T. ) ;
#13508=ADVANCED_FACE ( 'NONE', ( #12380 ), #3281, .F. ) ;
#13512=ORIENTED_EDGE ( 'NONE', *, *, #5470, .T. ) ;
#13542=AXIS2_PLACEMENT_3D ( 'NONE', #1692, #1789, #10627 ) ;
#13543=DIRECTION ( 'NONE',  ( 0.000000000000000000, 0.000000000000000000, -1.000000000000000000 ) ) ;
#13556=VECTOR ( 'NONE', #13367, 1000.000000000000000 ) ;
#13593=EDGE_CURVE ( 'NONE', #9116, #4106, #2827, .T. ) ;
#13604=EDGE_CURVE ( 'NONE', #12123, #9647, #13488, .T. ) ;
#13616=EDGE_CURVE ( 'NONE', #15821, #452, #2174, .T. ) ;
#13620=VECTOR ( 'NONE', #12065, 1000.000000000000000 ) ;
#13627=CARTESIAN_POINT ( 'NONE',  ( -21.00000000000002842, -20.00000000000000000, -34.99999999999999289 ) ) ;
#13633=LINE ( 'NONE', #822, #12533 ) ;
#13643=VECTOR ( 'NONE', #11971, 1000.000000000000000 ) ;
#13680=CARTESIAN_POINT ( 'NONE',  ( 35.00000000000003553, -20.00000000000000000, -20.99999999999999645 ) ) ;
#13703=CARTESIAN_POINT ( 'NONE',  ( 34.00000000000002842, 0.000000000000000000, 31.00000000000000000 ) ) ;
#13704=DIRECTION ( 'NONE',  ( 0.000000000000000000, 0.000000000000000000, 1.000000000000000000 ) ) ;
#13706=ORIENTED_EDGE ( 'NONE', *, *, #13593, .F. ) ;
#13719=LINE ( 'NONE', #8564, #646 ) ;
#13726=VERTEX_POINT ( 'NONE', #2209 ) ;
#13790=EDGE_LOOP ( 'NONE', ( #9756, #14889, #11914, #28 ) ) ;
#13796=VECTOR ( 'NONE', #13095, 1000.000000000000000 ) ;
#13797=AXIS2_PLACEMENT_3D ( 'NONE', #9710, #13489, #2922 ) ;
#13806=CARTESIAN_POINT ( 'NONE',  ( 20.99999999999996092, 3.000000000000000000, 35.00000000000000711 ) ) ;
#13814=ORIENTED_EDGE ( 'NONE', *, *, #2646, .F. ) ;
#13824=AXIS2_PLACEMENT_3D ( 'NONE', #14190, #7815, #6431 ) ;
#13839=EDGE_CURVE ( 'NONE', #15603, #3880, #16433, .T. ) ;
#13892=DIRECTION ( 'NONE',  ( 0.000000000000000000, 0.000000000000000000, 1.000000000000000000 ) ) ;
#13911=EDGE_CURVE ( 'NONE', #2045, #12055, #10376, .T. ) ;
#13915=CARTESIAN_POINT ( 'NONE',  ( 30.99999999999999645, 3.000000000000000000, -25.99999999999999645 ) ) ;
#13918=CARTESIAN_POINT ( 'NONE',  ( 30.99999999999999645, 3.000000000000000000, 26.00000000000000355 ) ) ;
#13929=ORIENTED_EDGE ( 'NONE', *, *, #15894, .F. ) ;
#13939=EDGE_LOOP ( 'NONE', ( #2327, #9873, #5401, #9685 ) ) ;
#13944=VERTEX_POINT ( 'NONE', #157 ) ;
#13948=EDGE_LOOP ( 'NONE', ( #8148, #4028, #16785, #7170 ) ) ;
#13949=DIRECTION ( 'NONE',  ( 0.000000000000000000, 0.000000000000000000, -1.000000000000000000 ) ) ;
#13951=DIRECTION ( 'NONE',  ( -0.000000000000000000, 1.000000000000000000, -0.000000000000000000 ) ) ;
#13968=DIRECTION ( 'NONE',  ( -0.000000000000000000, -1.000000000000000000, -0.000000000000000000 ) ) ;
#13988=CIRCLE ( 'NONE', #3571, 4.999999999999997335 ) ;
#14007=CARTESIAN_POINT ( 'NONE',  ( -26.00000000000002842, 0.000000000000000000, 34.00000000000000711 ) ) ;
#14048=AXIS2_PLACEMENT_3D ( 'NONE', #12286, #9874, #3184 ) ;
#14052=DIRECTION ( 'NONE',  ( -0.000000000000000000, -1.000000000000000000, -0.000000000000000000 ) ) ;
#14064=ORIENTED_EDGE ( 'NONE', *, *, #10037, .F. ) ;
#14069=AXIS2_PLACEMENT_3D ( 'NONE', #10257, #7833, #15575 ) ;
#14079=LINE ( 'NONE', #12869, #9848 ) ;
#14081=ORIENTED_EDGE ( 'NONE', *, *, #13604, .F. ) ;
#14082=LINE ( 'NONE', #11669, #1117 ) ;
#14088=VECTOR ( 'NONE', #4823, 1000.000000000000000 ) ;
#14096=CYLINDRICAL_SURFACE ( 'NONE', #9178, 3.000000000000002665 ) ;
#14114=EDGE_LOOP ( 'NONE', ( #13176, #12622, #6522, #9753 ) ) ;
#14128=EDGE_CURVE ( 'NONE', #12822, #9226, #16871, .T. ) ;
#14134=DIRECTION ( 'NONE',  ( 0.000000000000000000, 0.000000000000000000, 1.000000000000000000 ) ) ;
#14141=FACE_BOUND ( 'NONE', #10686, .T. ) ;
#14148=ADVANCED_FACE ( 'NONE', ( #3823 ), #2439, .F. ) ;
#14152=ADVANCED_FACE ( 'NONE', ( #8904, #14296, #2526, #7756, #14141, #13019 ), #1248, .F. ) ;
#14157=ORIENTED_EDGE ( 'NONE', *, *, #11283, .F. ) ;
#14169=DIRECTION ( 'NONE',  ( 0.000000000000000000, 1.000000000000000000, 0.000000000000000000 ) ) ;
#14174=CARTESIAN_POINT ( 'NONE',  ( 35.00000000000003553, -20.00000000000000000, -23.50000000000000000 ) ) ;
#14190=CARTESIAN_POINT ( 'NONE',  ( -34.99999999999998579, -20.00000000000000000, 21.00000000000000355 ) ) ;
#14208=DIRECTION ( 'NONE',  ( -0.000000000000000000, -0.000000000000000000, 1.000000000000000000 ) ) ;
#14210=CARTESIAN_POINT ( 'NONE',  ( 34.00000000000002842, 0.000000000000000000, 23.00000000000000355 ) ) ;
#14223=LINE ( 'NONE', #1002, #9426 ) ;
#14237=DIRECTION ( 'NONE',  ( 0.000000000000000000, 0.000000000000000000, 1.000000000000000000 ) ) ;
#14240=EDGE_CURVE ( 'NONE', #5928, #15603, #10517, .T. ) ;
#14274=CYLINDRICAL_SURFACE ( 'NONE', #14658, 34.00000000000000000 ) ;
#14275=VERTEX_POINT ( 'NONE', #2089 ) ;
#14277=ORIENTED_EDGE ( 'NONE', *, *, #6234, .T. ) ;
#14292=ORIENTED_EDGE ( 'NONE', *, *, #12106, .T. ) ;
#14296=FACE_BOUND ( 'NONE', #14563, .T. ) ;
#14301=ADVANCED_FACE ( 'NONE', ( #4742 ), #5707, .T. ) ;
#14305=CLOSED_SHELL ( 'NONE', ( #16738, #10690, #2984, #2238, #14301, #6830, #4024, #3497, #13508, #11439, #10543, #16121, #3815, #14148, #12119, #1414, #1535, #15809, #10335, #10929, #11486, #2699, #15193, #16334, #14456, #577, #3734, #9824, #6334, #14152, #11078, #14328, #6754, #14355, #6734, #13131, #6330, #14879, #3736, #382, #1829, #8158, #5162, #5491 ) ) ;
#14316=AXIS2_PLACEMENT_3D ( 'NONE', #7762, #16874, #5448 ) ;
#14328=ADVANCED_FACE ( 'NONE', ( #4653 ), #639, .T. ) ;
#14329=CYLINDRICAL_SURFACE ( 'NONE', #12307, 2.500000000000002220 ) ;
#14333=EDGE_CURVE ( 'NONE', #1391, #7963, #4588, .T. ) ;
#14343=VERTEX_POINT ( 'NONE', #14989 ) ;
#14355=ADVANCED_FACE ( 'NONE', ( #12487 ), #732, .F. ) ;
#14363=EDGE_LOOP ( 'NONE', ( #11972, #15730, #14507, #2416 ) ) ;
#14371=VERTEX_POINT ( 'NONE', #10393 ) ;
#14378=ORIENTED_EDGE ( 'NONE', *, *, #5423, .T. ) ;
#14398=CARTESIAN_POINT ( 'NONE',  ( -21.00000000000002842, 0.000000000000000000, -32.49999999999999289 ) ) ;
#14403=CARTESIAN_POINT ( 'NONE',  ( 30.99999999999995737, 3.000000000000000000, 31.00000000000000000 ) ) ;
#14421=LINE ( 'NONE', #6767, #9691 ) ;
#14431=EDGE_CURVE ( 'NONE', #1567, #6332, #10482, .T. ) ;
#14443=FACE_OUTER_BOUND ( 'NONE', #14695, .T. ) ;
#14456=ADVANCED_FACE ( 'NONE', ( #6420 ), #2575, .F. ) ;
#14460=EDGE_CURVE ( 'NONE', #13400, #1978, #8010, .T. ) ;
#14484=CARTESIAN_POINT ( 'NONE',  ( 30.99999999999999645, 0.000000000000000000, -25.99999999999999645 ) ) ;
#14488=DIRECTION ( 'NONE',  ( 0.000000000000000000, 1.000000000000000000, 0.000000000000000000 ) ) ;
#14506=CARTESIAN_POINT ( 'NONE',  ( 0.000000000000000000, 26.00000000000000000, -36.50000000000000000 ) ) ;
#14507=ORIENTED_EDGE ( 'NONE', *, *, #2051, .F. ) ;
#14513=CIRCLE ( 'NONE', #1381, 36.50000000000000000 ) ;
#14527=AXIS2_PLACEMENT_3D ( 'NONE', #5663, #14855, #11942 ) ;
#14541=CARTESIAN_POINT ( 'NONE',  ( -39.99999999999997868, 0.000000000000000000, -25.99999999999999645 ) ) ;
#14544=CARTESIAN_POINT ( 'NONE',  ( 30.99999999999997158, 0.000000000000000000, 19.99999999999999289 ) ) ;
#14546=VERTEX_POINT ( 'NONE', #4460 ) ;
#14551=EDGE_CURVE ( 'NONE', #5917, #16466, #7459, .T. ) ;
#14557=AXIS2_PLACEMENT_3D ( 'NONE', #16024, #1598, #7854 ) ;
#14563=EDGE_LOOP ( 'NONE', ( #8724, #4875 ) ) ;
#14565=CYLINDRICAL_SURFACE ( 'NONE', #12435, 2.500000000000002220 ) ;
#14575=CARTESIAN_POINT ( 'NONE',  ( 19.99999999999995381, 3.000000000000000000, -36.99999999999999289 ) ) ;
#14579=CARTESIAN_POINT ( 'NONE',  ( 25.99999999999996092, 3.000000000000000000, 40.00000000000000711 ) ) ;
#14591=CARTESIAN_POINT ( 'NONE',  ( -26.00000000000002842, 0.000000000000000000, -31.00000000000003197 ) ) ;
#14599=CARTESIAN_POINT ( 'NONE',  ( -31.00000000000002842, 3.000000000000000000, 31.00000000000000000 ) ) ;
#14610=ORIENTED_EDGE ( 'NONE', *, *, #8214, .F. ) ;
#14654=EDGE_CURVE ( 'NONE', #11956, #9226, #11235, .T. ) ;
#14656=CYLINDRICAL_SURFACE ( 'NONE', #14316, 4.999999999999997335 ) ;
#14658=AXIS2_PLACEMENT_3D ( 'NONE', #4986, #3879, #2495 ) ;
#14681=DIRECTION ( 'NONE',  ( 0.000000000000000000, 0.000000000000000000, -1.000000000000000000 ) ) ;
#14683=ORIENTED_EDGE ( 'NONE', *, *, #1019, .T. ) ;
#14686=DIRECTION ( 'NONE',  ( -0.000000000000000000, -1.000000000000000000, -0.000000000000000000 ) ) ;
#14687=DIRECTION ( 'NONE',  ( 1.000000000000000000, -0.000000000000000000, -0.000000000000000000 ) ) ;
#14695=EDGE_LOOP ( 'NONE', ( #5141, #1522, #16197, #9422 ) ) ;
#14708=CARTESIAN_POINT ( 'NONE',  ( 22.99999999999995737, 0.000000000000000000, -33.99999999999998579 ) ) ;
#14722=VERTEX_POINT ( 'NONE', #10205 ) ;
#14726=CARTESIAN_POINT ( 'NONE',  ( -39.99999999999997868, 0.000000000000000000, 26.00000000000000355 ) ) ;
#14749=DIRECTION ( 'NONE',  ( -0.000000000000000000, 1.000000000000000000, -0.000000000000000000 ) ) ;
#14774=EDGE_CURVE ( 'NONE', #1567, #13944, #11658, .T. ) ;
#14785=CARTESIAN_POINT ( 'NONE',  ( -26.00000000000002842, 0.000000000000000000, -39.99999999999999289 ) ) ;
#14800=ORIENTED_EDGE ( 'NONE', *, *, #14240, .F. ) ;
#14808=VECTOR ( 'NONE', #2737, 1000.000000000000000 ) ;
#14831=CARTESIAN_POINT ( 'NONE',  ( 19.99999999999995381, 3.000000000000000000, -36.99999999999999289 ) ) ;
#14847=CARTESIAN_POINT ( 'NONE',  ( 40.00000000000003553, 3.000000000000000000, -25.99999999999999645 ) ) ;
#14855=DIRECTION ( 'NONE',  ( -0.000000000000000000, -1.000000000000000000, 0.000000000000000000 ) ) ;
#14858=EDGE_LOOP ( 'NONE', ( #11576, #15820, #15303, #2023 ) ) ;
#14863=ORIENTED_EDGE ( 'NONE', *, *, #409, .T. ) ;
#14865=EDGE_CURVE ( 'NONE', #1506, #856, #2277, .T. ) ;
#14878=DIRECTION ( 'NONE',  ( 1.000000000000000000, 0.000000000000000000, -0.000000000000000000 ) ) ;
#14879=ADVANCED_FACE ( 'NONE', ( #8044 ), #5382, .F. ) ;
#14889=ORIENTED_EDGE ( 'NONE', *, *, #535, .T. ) ;
#14892=ORIENTED_EDGE ( 'NONE', *, *, #3017, .F. ) ;
#14900=DIRECTION ( 'NONE',  ( 0.000000000000000000, 0.000000000000000000, -1.000000000000000000 ) ) ;
#14905=CIRCLE ( 'NONE', #3928, 36.50000000000000000 ) ;
#14913=CARTESIAN_POINT ( 'NONE',  ( 0.000000000000000000, 3.000000000000000000, -36.50000000000000000 ) ) ;
#14941=VERTEX_POINT ( 'NONE', #14579 ) ;
#14949=FACE_BOUND ( 'NONE', #10276, .T. ) ;
#14966=PRODUCT ( 'Servo-Bas', 'Servo-Bas', '', ( #2069 ) ) ;
#14979=LINE ( 'NONE', #11021, #4483 ) ;
#14985=EDGE_CURVE ( 'NONE', #13726, #856, #13719, .T. ) ;
#14986=EDGE_CURVE ( 'NONE', #175, #9495, #16378, .T. ) ;
#14989=CARTESIAN_POINT ( 'NONE',  ( 34.00000000000002842, 3.000000000000000000, 23.00000000000000355 ) ) ;
#15018=DIRECTION ( 'NONE',  ( 1.000000000000000000, 0.000000000000000000, -0.000000000000000000 ) ) ;
#15034=LINE ( 'NONE', #8597, #11090 ) ;
#15035=ORIENTED_EDGE ( 'NONE', *, *, #10607, .T. ) ;
#15045=EDGE_LOOP ( 'NONE', ( #14157, #2776 ) ) ;
#15065=LINE ( 'NONE', #13703, #7481 ) ;
#15075=DIRECTION ( 'NONE',  ( 0.000000000000000000, 0.000000000000000000, 1.000000000000000000 ) ) ;
#15102=DIRECTION ( 'NONE',  ( 1.000000000000000000, 0.000000000000000000, 0.000000000000000000 ) ) ;
#15115=CARTESIAN_POINT ( 'NONE',  ( -20.00000000000003197, 3.000000000000000000, 37.00000000000000711 ) ) ;
#15121=CYLINDRICAL_SURFACE ( 'NONE', #12404, 2.500000000000002220 ) ;
#15130=DIRECTION ( 'NONE',  ( 0.000000000000000000, 0.000000000000000000, 1.000000000000000000 ) ) ;
#15144=CARTESIAN_POINT ( 'NONE',  ( -34.99999999999998579, 0.000000000000000000, 23.50000000000000711 ) ) ;
#15174=EDGE_LOOP ( 'NONE', ( #4801, #9927, #7905, #1297 ) ) ;
#15191=EDGE_CURVE ( 'NONE', #4106, #12123, #10242, .T. ) ;
#15193=ADVANCED_FACE ( 'NONE', ( #7507 ), #1334, .F. ) ;
#15195=EDGE_CURVE ( 'NONE', #687, #3292, #14223, .T. ) ;
#15211=ORIENTED_EDGE ( 'NONE', *, *, #3147, .T. ) ;
#15217=DIRECTION ( 'NONE',  ( 1.000000000000000000, 0.000000000000000000, 0.000000000000000000 ) ) ;
#15221=CARTESIAN_POINT ( 'NONE',  ( 0.000000000000000000, 16.00000000000000000, 0.000000000000000000 ) ) ;
#15228=VECTOR ( 'NONE', #14237, 1000.000000000000000 ) ;
#15242=CARTESIAN_POINT ( 'NONE',  ( -34.99999999999998579, 3.000000000000000000, 21.00000000000000355 ) ) ;
#15287=EDGE_CURVE ( 'NONE', #8217, #1389, #311, .T. ) ;
#15289=DIRECTION ( 'NONE',  ( -0.000000000000000000, -1.000000000000000000, -0.000000000000000000 ) ) ;
#15301=( LENGTH_UNIT ( ) NAMED_UNIT ( * ) SI_UNIT ( .MILLI., .METRE. ) );
#15303=ORIENTED_EDGE ( 'NONE', *, *, #12802, .T. ) ;
#15314=VERTEX_POINT ( 'NONE', #10779 ) ;
#15320=CIRCLE ( 'NONE', #7628, 4.999999999999997335 ) ;
#15325=DIRECTION ( 'NONE',  ( 0.000000000000000000, 0.000000000000000000, -1.000000000000000000 ) ) ;
#15346=CARTESIAN_POINT ( 'NONE',  ( -31.00000000000003197, 0.000000000000000000, -30.99999999999999289 ) ) ;
#15366=LINE ( 'NONE', #13918, #1818 ) ;
#15391=EDGE_LOOP ( 'NONE', ( #9118, #7794, #9713, #10495 ) ) ;
#15393=VECTOR ( 'NONE', #12652, 1000.000000000000000 ) ;
#15412=LINE ( 'NONE', #10268, #5769 ) ;
#15419=FACE_OUTER_BOUND ( 'NONE', #5801, .T. ) ;
#15431=AXIS2_PLACEMENT_3D ( 'NONE', #248, #3936, #14681 ) ;
#15457=EDGE_LOOP ( 'NONE', ( #16490, #5202, #2510, #11949 ) ) ;
#15458=AXIS2_PLACEMENT_3D ( 'NONE', #6260, #15558, #6512 ) ;
#15502=DIRECTION ( 'NONE',  ( 0.000000000000000000, 1.000000000000000000, 0.000000000000000000 ) ) ;
#15536=CARTESIAN_POINT ( 'NONE',  ( -21.00000000000002842, 0.000000000000000000, -37.50000000000000000 ) ) ;
#15558=DIRECTION ( 'NONE',  ( 1.000000000000000000, -0.000000000000000000, 0.000000000000000000 ) ) ;
#15575=DIRECTION ( 'NONE',  ( 0.000000000000000000, 0.000000000000000000, 1.000000000000000000 ) ) ;
#15588=DIRECTION ( 'NONE',  ( -0.000000000000000000, -1.000000000000000000, 0.000000000000000000 ) ) ;
#15590=DIRECTION ( 'NONE',  ( -0.000000000000000000, -1.000000000000000000, -0.000000000000000000 ) ) ;
#15598=CIRCLE ( 'NONE', #3531, 4.999999999999997335 ) ;
#15603=VERTEX_POINT ( 'NONE', #7736 ) ;
#15611=EDGE_CURVE ( 'NONE', #974, #11696, #8329, .T. ) ;
#15639=ORIENTED_EDGE ( 'NONE', *, *, #287, .T. ) ;
#15640=LINE ( 'NONE', #7818, #10261 ) ;
#15656=CARTESIAN_POINT ( 'NONE',  ( 25.99999999999996092, 3.000000000000000000, 31.00000000000004263 ) ) ;
#15659=DIRECTION ( 'NONE',  ( 0.000000000000000000, 1.000000000000000000, 0.000000000000000000 ) ) ;
#15662=CARTESIAN_POINT ( 'NONE',  ( 30.99999999999995737, 3.000000000000000000, 31.00000000000000000 ) ) ;
#15666=ORIENTED_EDGE ( 'NONE', *, *, #8143, .F. ) ;
#15667=CARTESIAN_POINT ( 'NONE',  ( -31.00000000000006395, 3.000000000000000000, -25.99999999999999645 ) ) ;
#15701=VECTOR ( 'NONE', #7953, 1000.000000000000000 ) ;
#15721=CIRCLE ( 'NONE', #14069, 2.999999999999995559 ) ;
#15730=ORIENTED_EDGE ( 'NONE', *, *, #5423, .F. ) ;
#15734=DIRECTION ( 'NONE',  ( 1.000000000000000000, -0.000000000000000000, 0.000000000000000000 ) ) ;
#15744=PLANE ( 'NONE',  #11175 ) ;
#15766=CARTESIAN_POINT ( 'NONE',  ( -26.00000000000002842, 0.000000000000000000, 31.00000000000003908 ) ) ;
#15775=CARTESIAN_POINT ( 'NONE',  ( -20.00000000000003197, 3.000000000000000000, 37.00000000000000711 ) ) ;
#15780=EDGE_CURVE ( 'NONE', #452, #9574, #5242, .T. ) ;
#15783=EDGE_LOOP ( 'NONE', ( #9877, #10726, #2191, #16541 ) ) ;
#15793=VECTOR ( 'NONE', #5580, 1000.000000000000000 ) ;
#15795=EDGE_CURVE ( 'NONE', #2045, #175, #27, .T. ) ;
#15797=EDGE_LOOP ( 'NONE', ( #2384, #4078, #3619, #10071 ) ) ;
#15809=ADVANCED_FACE ( 'NONE', ( #371 ), #2946, .F. ) ;
#15820=ORIENTED_EDGE ( 'NONE', *, *, #3017, .T. ) ;
#15821=VERTEX_POINT ( 'NONE', #6614 ) ;
#15828=DIRECTION ( 'NONE',  ( -0.000000000000000000, 1.000000000000000000, -0.000000000000000000 ) ) ;
#15833=LINE ( 'NONE', #9309, #201 ) ;
#15854=ORIENTED_EDGE ( 'NONE', *, *, #13194, .T. ) ;
#15857=LINE ( 'NONE', #15775, #582 ) ;
#15861=DIRECTION ( 'NONE',  ( -0.000000000000000000, -1.000000000000000000, 0.000000000000000000 ) ) ;
#15864=EDGE_LOOP ( 'NONE', ( #4667, #1123, #12896, #11022 ) ) ;
#15871=DIRECTION ( 'NONE',  ( 0.000000000000000000, 0.000000000000000000, 1.000000000000000000 ) ) ;
#15894=EDGE_CURVE ( 'NONE', #5917, #9633, #9649, .T. ) ;
#15899=CARTESIAN_POINT ( 'NONE',  ( -26.00000000000002842, 0.000000000000000000, 34.00000000000000711 ) ) ;
#15901=EDGE_LOOP ( 'NONE', ( #9191, #7499, #2623, #6913 ) ) ;
#15937=ORIENTED_EDGE ( 'NONE', *, *, #1524, .T. ) ;
#15939=VECTOR ( 'NONE', #5623, 1000.000000000000000 ) ;
#15944=( GEOMETRIC_REPRESENTATION_CONTEXT ( 3 ) GLOBAL_UNCERTAINTY_ASSIGNED_CONTEXT ( ( #523 ) ) GLOBAL_UNIT_ASSIGNED_CONTEXT ( ( #13317, #9532, #6581 ) ) REPRESENTATION_CONTEXT ( 'NONE', 'WORKASPACE' ) );
#15952=CARTESIAN_POINT ( 'NONE',  ( 40.00000000000003553, 0.000000000000000000, 20.00000000000000355 ) ) ;
#15961=AXIS2_PLACEMENT_3D ( 'NONE', #10000, #3048, #7321 ) ;
#15964=VECTOR ( 'NONE', #4389, 1000.000000000000000 ) ;
#15967=CARTESIAN_POINT ( 'NONE',  ( -21.00000000000002842, -20.00000000000000000, -32.49999999999999289 ) ) ;
#15976=ORIENTED_EDGE ( 'NONE', *, *, #16846, .F. ) ;
#16024=CARTESIAN_POINT ( 'NONE',  ( -21.00000000000002842, -20.00000000000000000, -34.99999999999999289 ) ) ;
#16028=CARTESIAN_POINT ( 'NONE',  ( 25.99999999999996092, 3.000000000000000000, 40.00000000000000711 ) ) ;
#16031=DIRECTION ( 'NONE',  ( 0.000000000000000000, 0.000000000000000000, -1.000000000000000000 ) ) ;
#16041=CARTESIAN_POINT ( 'NONE',  ( 30.99999999999996092, 0.000000000000000000, -30.99999999999999289 ) ) ;
#16062=FACE_OUTER_BOUND ( 'NONE', #5802, .T. ) ;
#16066=CARTESIAN_POINT ( 'NONE',  ( -39.99999999999997868, 3.000000000000000000, -19.99999999999999645 ) ) ;
#16069=ORIENTED_EDGE ( 'NONE', *, *, #15191, .F. ) ;
#16098=ORIENTED_EDGE ( 'NONE', *, *, #14986, .T. ) ;
#16104=CARTESIAN_POINT ( 'NONE',  ( -26.00000000000002842, 3.000000000000000000, -39.99999999999999289 ) ) ;
#16110=DIRECTION ( 'NONE',  ( -0.000000000000000000, 1.000000000000000000, -0.000000000000000000 ) ) ;
#16120=EDGE_CURVE ( 'NONE', #8714, #14722, #7461, .T. ) ;
#16121=ADVANCED_FACE ( 'NONE', ( #8856 ), #14096, .F. ) ;
#16127=CARTESIAN_POINT ( 'NONE',  ( 25.99999999999996092, 3.000000000000000000, -31.00000000000003197 ) ) ;
#16131=CARTESIAN_POINT ( 'NONE',  ( -34.99999999999998579, -20.00000000000000000, 23.50000000000000711 ) ) ;
#16132=CIRCLE ( 'NONE', #9275, 2.999999999999995559 ) ;
#16138=ORIENTED_EDGE ( 'NONE', *, *, #14460, .F. ) ;
#16158=ORIENTED_EDGE ( 'NONE', *, *, #10271, .T. ) ;
#16165=LINE ( 'NONE', #4144, #16801 ) ;
#16180=CIRCLE ( 'NONE', #12893, 2.500000000000002220 ) ;
#16188=DIRECTION ( 'NONE',  ( 0.000000000000000000, 1.000000000000000000, 0.000000000000000000 ) ) ;
#16189=CARTESIAN_POINT ( 'NONE',  ( 34.00000000000002842, -20.00000000000000000, 23.00000000000000355 ) ) ;
#16197=ORIENTED_EDGE ( 'NONE', *, *, #13911, .T. ) ;
#16206=ORIENTED_EDGE ( 'NONE', *, *, #6664, .F. ) ;
#16208=DIRECTION ( 'NONE',  ( 0.000000000000000000, 0.000000000000000000, 1.000000000000000000 ) ) ;
#16245=EDGE_LOOP ( 'NONE', ( #10028, #3817 ) ) ;
#16248=CIRCLE ( 'NONE', #3900, 34.00000000000000000 ) ;
#16274=CARTESIAN_POINT ( 'NONE',  ( -39.99999999999997868, 3.000000000000000000, -25.99999999999999645 ) ) ;
#16291=VECTOR ( 'NONE', #13286, 1000.000000000000000 ) ;
#16296=VECTOR ( 'NONE', #8427, 1000.000000000000000 ) ;
#16307=PLANE ( 'NONE',  #13314 ) ;
#16325=ORIENTED_EDGE ( 'NONE', *, *, #7546, .F. ) ;
#16326=ORIENTED_EDGE ( 'NONE', *, *, #287, .F. ) ;
#16334=ADVANCED_FACE ( 'NONE', ( #9857 ), #1006, .F. ) ;
#16347=ORIENTED_EDGE ( 'NONE', *, *, #10667, .T. ) ;
#16353=ORIENTED_EDGE ( 'NONE', *, *, #14865, .F. ) ;
#16378=LINE ( 'NONE', #5897, #8605 ) ;
#16401=LINE ( 'NONE', #4472, #9576 ) ;
#16422=EDGE_CURVE ( 'NONE', #1391, #9705, #1717, .T. ) ;
#16433=CIRCLE ( 'NONE', #9037, 36.50000000000000000 ) ;
#16448=EDGE_LOOP ( 'NONE', ( #8296, #5732, #16599, #7990 ) ) ;
#16466=VERTEX_POINT ( 'NONE', #14398 ) ;
#16490=ORIENTED_EDGE ( 'NONE', *, *, #3216, .F. ) ;
#16536=CARTESIAN_POINT ( 'NONE',  ( 30.99999999999999645, 3.000000000000000000, 26.00000000000000355 ) ) ;
#16541=ORIENTED_EDGE ( 'NONE', *, *, #12459, .T. ) ;
#16545=CARTESIAN_POINT ( 'NONE',  ( -36.99999999999997868, 3.000000000000000000, -22.99999999999999645 ) ) ;
#16563=VECTOR ( 'NONE', #1574, 1000.000000000000000 ) ;
#16597=ORIENTED_EDGE ( 'NONE', *, *, #14551, .F. ) ;
#16598=ORIENTED_EDGE ( 'NONE', *, *, #10271, .F. ) ;
#16599=ORIENTED_EDGE ( 'NONE', *, *, #521, .T. ) ;
#16600=DIRECTION ( 'NONE',  ( 0.000000000000000000, -1.000000000000000000, 0.000000000000000000 ) ) ;
#16603=DIRECTION ( 'NONE',  ( 0.000000000000000000, 0.000000000000000000, -1.000000000000000000 ) ) ;
#16608=DIRECTION ( 'NONE',  ( -0.000000000000000000, -1.000000000000000000, -0.000000000000000000 ) ) ;
#16613=CARTESIAN_POINT ( 'NONE',  ( 25.99999999999996092, 0.000000000000000000, -31.00000000000003197 ) ) ;
#16656=VERTEX_POINT ( 'NONE', #4089 ) ;
#16683=EDGE_CURVE ( 'NONE', #10598, #11589, #12074, .T. ) ;
#16694=ORIENTED_EDGE ( 'NONE', *, *, #15195, .F. ) ;
#16697=DIRECTION ( 'NONE',  ( 1.000000000000000000, 0.000000000000000000, -0.000000000000000000 ) ) ;
#16716=EDGE_CURVE ( 'NONE', #7341, #6882, #4351, .T. ) ;
#16730=CARTESIAN_POINT ( 'NONE',  ( -39.99999999999997868, 3.000000000000000000, 26.00000000000000355 ) ) ;
#16738=ADVANCED_FACE ( 'NONE', ( #3152 ), #14565, .F. ) ;
#16754=EDGE_LOOP ( 'NONE', ( #16864, #4395, #4646, #12916 ) ) ;
#16785=ORIENTED_EDGE ( 'NONE', *, *, #67, .F. ) ;
#16801=VECTOR ( 'NONE', #1576, 1000.000000000000000 ) ;
#16822=( GEOMETRIC_REPRESENTATION_CONTEXT ( 3 ) GLOBAL_UNCERTAINTY_ASSIGNED_CONTEXT ( ( #10188 ) ) GLOBAL_UNIT_ASSIGNED_CONTEXT ( ( #15301, #12721, #8604 ) ) REPRESENTATION_CONTEXT ( 'NONE', 'WORKASPACE' ) );
#16826=CARTESIAN_POINT ( 'NONE',  ( -34.99999999999998579, -20.00000000000000000, 18.50000000000000355 ) ) ;
#16831=DIRECTION ( 'NONE',  ( -0.000000000000000000, -1.000000000000000000, -0.000000000000000000 ) ) ;
#16835=EDGE_CURVE ( 'NONE', #12822, #8007, #15065, .T. ) ;
#16846=EDGE_CURVE ( 'NONE', #15314, #14722, #379, .T. ) ;
#16863=LINE ( 'NONE', #15656, #11798 ) ;
#16864=ORIENTED_EDGE ( 'NONE', *, *, #7342, .T. ) ;
#16871=LINE ( 'NONE', #9060, #11579 ) ;
#16874=DIRECTION ( 'NONE',  ( -0.000000000000000000, -1.000000000000000000, -0.000000000000000000 ) ) ;
#16899=FILL_AREA_STYLE_COLOUR ( '', #7134 ) ;
#16943=PLANE ( 'NONE',  #449 ) ;
#16945=EDGE_LOOP ( 'NONE', ( #15854, #5420 ) ) ;
ENDSEC;
END-ISO-10303-21;
